ISO-10303-21;
HEADER;
FILE_DESCRIPTION (('STEP AP214'),
    '1' );
FILE_NAME ('hex flange nut gradea_iso_ISO - 4161 - M10 - N.step',
    '2026-10-08T07:58:12',
    ( '' ),
    ( '' ),
    'SwSTEP 2.0',
    'SolidWorks 2026',
    '' );
FILE_SCHEMA (( 'AUTOMOTIVE_DESIGN' ));
ENDSEC;

DATA;
#88=ORIENTED_EDGE ( 'NONE', *, *, #21349, .T. ) ;
#89=CARTESIAN_POINT ( 'NONE',  ( 5.147825380264231754, 5.688155668806028409, -7.450218641347809090 ) ) ;
#94=PRESENTATION_STYLE_ASSIGNMENT (( #8103 ) ) ;
#100=CARTESIAN_POINT ( 'NONE',  ( -7.500000000000000000, 4.330127018922191873, -7.422398894150032511 ) ) ;
#129=FACE_OUTER_BOUND ( 'NONE', #16222, .T. ) ;
#159=ORIENTED_EDGE ( 'NONE', *, *, #2470, .T. ) ;
#212=EDGE_CURVE ( 'NONE', #5261, #24452, #30622, .T. ) ;
#233=AXIS2_PLACEMENT_3D ( 'NONE', #28448, #5105, #25888 ) ;
#264=( NAMED_UNIT ( * ) PLANE_ANGLE_UNIT ( ) SI_UNIT ( $, .RADIAN. ) );
#331=CARTESIAN_POINT ( 'NONE',  ( -7.922281120364393914, -4.573931137438277617, -8.047472243342932430 ) ) ;
#350=CARTESIAN_POINT ( 'NONE',  ( -7.499999999999999112, -2.930060224340425901, -0.4701183149080249146 ) ) ;
#392=DIRECTION ( 'NONE',  ( 0.000000000000000000, 0.000000000000000000, 1.000000000000000000 ) ) ;
#407=AXIS2_PLACEMENT_3D ( 'NONE', #13866, #6364, #3304 ) ;
#435=ADVANCED_FACE ( 'NONE', ( #11935 ), #14477, .T. ) ;
#442=CARTESIAN_POINT ( 'NONE',  ( -5.000000000000000888, 6.123233995736767268E-16, -25.03750572909317285 ) ) ;
#467=AXIS2_PLACEMENT_3D ( 'NONE', #16628, #11526, #21908 ) ;
#478=CARTESIAN_POINT ( 'NONE',  ( 7.908217798048221781, 3.084840533507044125, -7.795645399445156443 ) ) ;
#511=CARTESIAN_POINT ( 'NONE',  ( 5.276765049035074817, -6.073111908730307817, -7.634085501268428331 ) ) ;
#566=CARTESIAN_POINT ( 'NONE',  ( -2.411464220262952818, -7.267994521134228059, -7.491772860715828486 ) ) ;
#613=VERTEX_POINT ( 'NONE', #8175 ) ;
#662=FACE_OUTER_BOUND ( 'NONE', #15822, .T. ) ;
#667=CARTESIAN_POINT ( 'NONE',  ( 4.613983237546155358, -6.452243898629820507, -7.591546097228409451 ) ) ;
#726=EDGE_LOOP ( 'NONE', ( #4770, #12905, #31541, #10132, #32533 ) ) ;
#746=CARTESIAN_POINT ( 'NONE',  ( 7.500000000000000000, -1.486698507076798847, -0.09861472150523931113 ) ) ;
#850=CARTESIAN_POINT ( 'NONE',  ( -7.500000000000000888, 2.886751345948126435, -7.198902722707427593 ) ) ;
#854=VERTEX_POINT ( 'NONE', #11721 ) ;
#879=CARTESIAN_POINT ( 'NONE',  ( 7.500000000000000888, 1.443375672974060109, -7.063244554130000630 ) ) ;
#920=AXIS2_PLACEMENT_3D ( 'NONE', #13262, #15985, #26700 ) ;
#948=VERTEX_POINT ( 'NONE', #16827 ) ;
#963=CARTESIAN_POINT ( 'NONE',  ( 6.250000000000000888, 5.051814855409225480, -7.198902722707425816 ) ) ;
#967=CARTESIAN_POINT ( 'NONE',  ( 7.500000000000000000, 3.948247735265829395, -7.349893093595813554 ) ) ;
#1036=CIRCLE ( 'NONE', #9747, 10.12668159690567649 ) ;
#1053=CARTESIAN_POINT ( 'NONE',  ( 7.500000000000000888, 3.608439182435154269, -7.298562697733103732 ) ) ;
#1084=DIRECTION ( 'NONE',  ( -1.000000000000000000, 0.000000000000000000, 0.000000000000000000 ) ) ;
#1131=CARTESIAN_POINT ( 'NONE',  ( 7.922281120364393914, -4.573931137438282057, -8.047472243342932430 ) ) ;
#1176=EDGE_CURVE ( 'NONE', #2927, #16155, #28150, .T. ) ;
#1208=ADVANCED_FACE ( 'NONE', ( #129 ), #14425, .F. ) ;
#1212=CARTESIAN_POINT ( 'NONE',  ( 7.500000000000000000, -3.608439182435168036, -7.298562697733107285 ) ) ;
#1221=B_SPLINE_CURVE_WITH_KNOTS ( 'NONE', 3,
 ( #24822, #19875, #11540, #6432, #4039, #6078, #21925, #16476, #22095, #32146 ),
 .UNSPECIFIED., .F., .F.,
 ( 4, 2, 2, 2, 4 ),
 ( 1.572453990175171705E-19, 0.002305503304226491201, 0.004611006608452982401, 0.006916509912679473168, 0.009222013216905964803 ),
 .UNSPECIFIED. ) ;
#1360=B_SPLINE_CURVE_WITH_KNOTS ( 'NONE', 3,
 ( #19450, #17063, #27787, #6512, #16723, #24567, #11623, #27126, #17401, #27615 ),
 .UNSPECIFIED., .F., .F.,
 ( 4, 2, 2, 2, 4 ),
 ( 0.000000000000000000, 0.002305503304226491634, 0.004611006608452983269, 0.006916509912679474036, 0.009222013216905963068 ),
 .UNSPECIFIED. ) ;
#1448=AXIS2_PLACEMENT_3D ( 'NONE', #12317, #22712, #9769 ) ;
#1489=ORIENTED_EDGE ( 'NONE', *, *, #4823, .T. ) ;
#1562=AXIS2_PLACEMENT_3D ( 'NONE', #7257, #10331, #18155 ) ;
#1569=EDGE_CURVE ( 'NONE', #4633, #19912, #4976, .T. ) ;
#1597=CARTESIAN_POINT ( 'NONE',  ( -7.970070017554212960, 4.546953124339755625, -8.057670357645356773 ) ) ;
#1626=CARTESIAN_POINT ( 'NONE',  ( -7.500000000000000000, 1.854554393013821745, -0.1880126015361722192 ) ) ;
#1632=PLANE ( 'NONE',  #19178 ) ;
#1732=AXIS2_PLACEMENT_3D ( 'NONE', #9905, #7356, #27280 ) ;
#1759=CARTESIAN_POINT ( 'NONE',  ( -7.298354728638373423, 4.926141412641537265, -7.913704048100170141 ) ) ;
#1797=EDGE_CURVE ( 'NONE', #31418, #32263, #7015, .T. ) ;
#1841=LINE ( 'NONE', #32841, #7687 ) ;
#1869=COLOUR_RGB ( '', 0.72549020, 0.75294118, 0.79215686) ;
#1921=CARTESIAN_POINT ( 'NONE',  ( -3.093157300003891663, -6.874418838041293611, -6.051203375184721622E-15 ) ) ;
#1930=FACE_OUTER_BOUND ( 'NONE', #19675, .T. ) ;
#1964=DIRECTION ( 'NONE',  ( -0.000000000000000000, -0.000000000000000000, 1.000000000000000000 ) ) ;
#1974=DIRECTION ( 'NONE',  ( 0.000000000000000000, 0.000000000000000000, 1.000000000000000000 ) ) ;
#1980=B_SPLINE_CURVE_WITH_KNOTS ( 'NONE', 3,
 ( #7965, #28407, #15284, #22954, #18350, #10189 ),
 .UNSPECIFIED., .F., .F.,
 ( 4, 2, 4 ),
 ( 0.004444412883774350592, 0.006655097293744440673, 0.008865781703714530754 ),
 .UNSPECIFIED. ) ;
#1999=VERTEX_POINT ( 'NONE', #16875 ) ;
#2075=CARTESIAN_POINT ( 'NONE',  ( -0.6249999999999991118, -8.299410119600880265, -7.298562697733108173 ) ) ;
#2088=ORIENTED_EDGE ( 'NONE', *, *, #12049, .F. ) ;
#2094=EDGE_CURVE ( 'NONE', #2685, #8055, #18977, .T. ) ;
#2109=EDGE_CURVE ( 'NONE', #32263, #5261, #11359, .T. ) ;
#2115=CARTESIAN_POINT ( 'NONE',  ( -7.112481253775184697, 4.553861071372892866, -7.781689322728085223 ) ) ;
#2189=DIRECTION ( 'NONE',  ( -1.000000000000000000, 0.000000000000000000, 0.000000000000000000 ) ) ;
#2225=DIRECTION ( 'NONE',  ( 0.000000000000000000, 0.000000000000000000, 1.000000000000000000 ) ) ;
#2254=ADVANCED_FACE ( 'NONE', ( #33402 ), #4825, .T. ) ;
#2277=CARTESIAN_POINT ( 'NONE',  ( -4.419133455862249704, 6.108866147517435508, -7.026396753507433424 ) ) ;
#2302=EDGE_CURVE ( 'NONE', #4633, #31418, #30982, .T. ) ;
#2404=AXIS2_PLACEMENT_3D ( 'NONE', #8872, #11941, #4266 ) ;
#2470=EDGE_CURVE ( 'NONE', #11897, #12741, #3041, .T. ) ;
#2523=CARTESIAN_POINT ( 'NONE',  ( 7.908030677224553884, -3.059924800338349904, -7.792662696733364314 ) ) ;
#2538=ADVANCED_FACE ( 'NONE', ( #20623 ), #13438, .T. ) ;
#2566=DIRECTION ( 'NONE',  ( -0.000000000000000000, -0.000000000000000000, 1.000000000000000000 ) ) ;
#2571=DIRECTION ( 'NONE',  ( 1.000000000000000000, 0.000000000000000000, 0.000000000000000000 ) ) ;
#2572=AXIS2_PLACEMENT_3D ( 'NONE', #3204, #8166, #26209 ) ;
#2583=AXIS2_PLACEMENT_3D ( 'NONE', #27846, #1964, #30933 ) ;
#2656=FILL_AREA_STYLE ('',( #31433 ) ) ;
#2663=CARTESIAN_POINT ( 'NONE',  ( -2.500000000000000000, 7.216878364870324525, -7.063244554130001518 ) ) ;
#2672=ADVANCED_FACE ( 'NONE', ( #5115 ), #23962, .F. ) ;
#2685=VERTEX_POINT ( 'NONE', #20952 ) ;
#2704=FACE_OUTER_BOUND ( 'NONE', #11685, .T. ) ;
#2742=CARTESIAN_POINT ( 'NONE',  ( -0.6508621380849236582, -8.763657152406455708, -7.907633014911225722 ) ) ;
#2806=ORIENTED_EDGE ( 'NONE', *, *, #14161, .F. ) ;
#2841=( BOUNDED_SURFACE ( )  B_SPLINE_SURFACE ( 3, 2, ( 
 ( #25300, #4516, #14908 ),
 ( #22750, #20187, #13033 ),
 ( #10652, #89, #18481 ),
 ( #3297, #23425, #26144 ),
 ( #15749, #10488, #18641 ),
 ( #18976, #21523, #13681 ),
 ( #16248, #13193, #21191 ),
 ( #5688, #20867, #31749 ) ),
 .UNSPECIFIED., .F., .F., .T. ) 
 B_SPLINE_SURFACE_WITH_KNOTS ( ( 4, 2, 2, 4 ),
 ( 3, 3 ),
 ( 0.03861844051980969222, 0.04325213341840641185, 0.04556897986770477166, 0.04788582631700313147 ),
 ( 0.000000000000000000, 1.000000000000000000 ),
 .UNSPECIFIED. ) 
 GEOMETRIC_REPRESENTATION_ITEM ( )  RATIONAL_B_SPLINE_SURFACE ( (
 ( 1.000000000000000000, 0.8047781759831921233, 1.000000000000000000),
 ( 1.000000000000000000, 0.8123762462806503049, 1.000000000000000000),
 ( 1.000000000000000000, 0.8190659850614813164, 1.000000000000000000),
 ( 1.000000000000000000, 0.8191937571014595854, 1.000000000000000000),
 ( 1.000000000000000000, 0.8176092952779865364, 1.000000000000000000),
 ( 1.000000000000000000, 0.8122962088597069918, 1.000000000000000000),
 ( 1.000000000000000000, 0.8086311330827506971, 1.000000000000000000),
 ( 1.000000000000000000, 0.8047712282214323221, 1.000000000000000000) ) ) 
 REPRESENTATION_ITEM ( '' )  SURFACE ( )  );
#2883=EDGE_CURVE ( 'NONE', #25547, #11897, #18841, .T. ) ;
#2909=ADVANCED_FACE ( 'NONE', ( #3219 ), #15259, .F. ) ;
#2927=VERTEX_POINT ( 'NONE', #4733 ) ;
#2971=DIRECTION ( 'NONE',  ( 1.000000000000000000, 0.000000000000000000, 0.000000000000000000 ) ) ;
#2980=CARTESIAN_POINT ( 'NONE',  ( 5.000000000000001776, 6.123233995736768255E-16, -9.974600000000000577 ) ) ;
#3018=DIRECTION ( 'NONE',  ( 0.000000000000000000, 0.000000000000000000, -1.000000000000000000 ) ) ;
#3041=B_SPLINE_CURVE_WITH_KNOTS ( 'NONE', 3,
 ( #12955, #2742, #28293, #28951, #17899, #13279, #23175, #26223, #23671, #331 ),
 .UNSPECIFIED., .F., .F.,
 ( 4, 2, 2, 2, 4 ),
 ( 0.000000000000000000, 0.002305503304226489900, 0.004611006608452982401, 0.006916509912679474036, 0.009222013216905966537 ),
 .UNSPECIFIED. ) ;
#3112=DIRECTION ( 'NONE',  ( 1.000000000000000000, 0.000000000000000000, 0.000000000000000000 ) ) ;
#3133=EDGE_CURVE ( 'NONE', #22909, #30882, #1841, .T. ) ;
#3169=CARTESIAN_POINT ( 'NONE',  ( -2.249192934210769784E-14, 9.016154170237596688, -7.999534413642735764 ) ) ;
#3190=CARTESIAN_POINT ( 'NONE',  ( 3.750000000000005329, 6.495190528383288253, 0.000000000000000000 ) ) ;
#3194=CARTESIAN_POINT ( 'NONE',  ( 7.897825807688775512, 1.532833846124499910, -7.633607627188418121 ) ) ;
#3204=CARTESIAN_POINT ( 'NONE',  ( -14.99999999999998934, -1.734723475976807094E-15, 0.000000000000000000 ) ) ;
#3219=FACE_OUTER_BOUND ( 'NONE', #30584, .T. ) ;
#3231=CARTESIAN_POINT ( 'NONE',  ( 7.970070017554212960, -4.546953124339766283, -8.057670357645358550 ) ) ;
#3265=ADVANCED_FACE ( 'NONE', ( #28250 ), #4414, .T. ) ;
#3267=CARTESIAN_POINT ( 'NONE',  ( -7.549004593702462351, -4.358419834287841965, -7.700121441565841884 ) ) ;
#3296=ORIENTED_EDGE ( 'NONE', *, *, #9534, .T. ) ;
#3297=CARTESIAN_POINT ( 'NONE',  ( 3.080866544135574259, 6.881514909250401324, -7.026396753507782478 ) ) ;
#3304=DIRECTION ( 'NONE',  ( -1.000000000000000000, 0.000000000000000000, 0.000000000000000000 ) ) ;
#3305=ADVANCED_FACE ( 'NONE', ( #15472 ), #9294, .T. ) ;
#3317=EDGE_LOOP ( 'NONE', ( #12594, #14639, #9064 ) ) ;
#3329=CARTESIAN_POINT ( 'NONE',  ( -6.127431526422343306E-17, 9.147862274876549904, -8.047472243342932430 ) ) ;
#3335=AXIS2_PLACEMENT_3D ( 'NONE', #12117, #27449, #14495 ) ;
#3336=B_SPLINE_CURVE_WITH_KNOTS ( 'NONE', 3,
 ( #16706, #32047, #8710, #16537, #24549, #26934 ),
 .UNSPECIFIED., .F., .F.,
 ( 4, 2, 4 ),
 ( 0.000000000000000000, 0.0004189869898914161677, 0.0008379739797828302753 ),
 .UNSPECIFIED. ) ;
#3383=CARTESIAN_POINT ( 'NONE',  ( 6.601567268551444378, -5.319966374295973743, -7.792327460285856766 ) ) ;
#3422=CARTESIAN_POINT ( 'NONE',  ( 7.500000000000007105, -4.330127018922196314, -7.564338275809341816 ) ) ;
#3469=B_SPLINE_CURVE_WITH_KNOTS ( 'NONE', 3,
 ( #28829, #26110, #12821, #23043, #20318, #5319, #33439, #25769, #8057, #15209 ),
 .UNSPECIFIED., .F., .F.,
 ( 4, 2, 2, 2, 4 ),
 ( 0.01051144076094935251, 0.01162027323572611265, 0.01272910571050287452, 0.01383793818527963640, 0.01494677066005639827 ),
 .UNSPECIFIED. ) ;
#3484=ADVANCED_FACE ( 'NONE', ( #2704 ), #25862, .F. ) ;
#3521=CARTESIAN_POINT ( 'NONE',  ( 7.499999999999999112, -1.614186302720606481, -7.450236204328171574 ) ) ;
#3564=CARTESIAN_POINT ( 'NONE',  ( 2.325424218458714165, -7.317669739337183898, -7.030005583191490715 ) ) ;
#3591=CARTESIAN_POINT ( 'NONE',  ( 7.549006887134069643, -4.358421158401204032, -7.700127545397312367 ) ) ;
#3592=CYLINDRICAL_SURFACE ( 'NONE', #4743, 5.000000000000000888 ) ;
#3609=ORIENTED_EDGE ( 'NONE', *, *, #9534, .F. ) ;
#3614=CARTESIAN_POINT ( 'NONE',  ( 3.749999999999999112, -6.495190528383302464, -6.991905250253757309 ) ) ;
#3624=VERTEX_POINT ( 'NONE', #21241 ) ;
#3676=VECTOR ( 'NONE', #7219, 1000.000000000000114 ) ;
#3684=CARTESIAN_POINT ( 'NONE',  ( -2.352990130084580066E-16, 8.660254037844390851, -7.422398894150034288 ) ) ;
#3700=ADVANCED_FACE ( 'NONE', ( #24769 ), #6027, .T. ) ;
#3704=ORIENTED_EDGE ( 'NONE', *, *, #20300, .T. ) ;
#3728=VECTOR ( 'NONE', #6069, 1000.000000000000114 ) ;
#3734=CARTESIAN_POINT ( 'NONE',  ( 6.486836893983020325, -4.915077010914103539, -7.231838333420563814 ) ) ;
#3746=AXIS2_PLACEMENT_3D ( 'NONE', #31280, #33662, #7940 ) ;
#3795=CARTESIAN_POINT ( 'NONE',  ( -7.897836333153808397, -1.530409084195006653, -7.633857274177628938 ) ) ;
#3844=CARTESIAN_POINT ( 'NONE',  ( 3.750000000000004441, -6.495190528383289141, 0.000000000000000000 ) ) ;
#3914=VECTOR ( 'NONE', #5288, 1000.000000000000114 ) ;
#3944=( GEOMETRIC_REPRESENTATION_CONTEXT ( 3 ) GLOBAL_UNCERTAINTY_ASSIGNED_CONTEXT ( ( #11468 ) ) GLOBAL_UNIT_ASSIGNED_CONTEXT ( ( #13039, #264, #33654 ) ) REPRESENTATION_CONTEXT ( 'NONE', 'WORKASPACE' ) );
#3958=B_SPLINE_CURVE_WITH_KNOTS ( 'NONE', 3,
 ( #12618, #33410, #23359, #31192, #18243, #28632 ),
 .UNSPECIFIED., .F., .F.,
 ( 4, 2, 4 ),
 ( 2.475503369207376426E-07, 0.002222330217055627170, 0.004444412883774334112 ),
 .UNSPECIFIED. ) ;
#4012=ORIENTED_EDGE ( 'NONE', *, *, #12277, .F. ) ;
#4022=FACE_OUTER_BOUND ( 'NONE', #10720, .T. ) ;
#4039=CARTESIAN_POINT ( 'NONE',  ( 3.280815508853482498, 7.221948645665444921, -7.591546097228400569 ) ) ;
#4144=CARTESIAN_POINT ( 'NONE',  ( -4.406466114815342117, 6.116179640280717145, -7.446478553995464544 ) ) ;
#4171=ORIENTED_EDGE ( 'NONE', *, *, #2883, .T. ) ;
#4262=VECTOR ( 'NONE', #22418, 1000.000000000000114 ) ;
#4266=DIRECTION ( 'NONE',  ( 1.000000000000000000, 0.000000000000000000, 0.000000000000000000 ) ) ;
#4275=DIRECTION ( 'NONE',  ( -0.000000000000000000, -0.000000000000000000, 1.000000000000000000 ) ) ;
#4361=CARTESIAN_POINT ( 'NONE',  ( -7.500000000000000000, 4.330127018922191873, -7.422398894150032511 ) ) ;
#4385=LINE ( 'NONE', #22439, #15693 ) ;
#4404=CARTESIAN_POINT ( 'NONE',  ( 0.000000000000000000, 0.000000000000000000, -0.5251556536572846712 ) ) ;
#4414=TOROIDAL_SURFACE ( 'NONE', #8240, 10.12668159690567649, 0.7733184030943209830 ) ;
#4452=CARTESIAN_POINT ( 'NONE',  ( -1.250000000000000444, -7.938566201357367902, -7.198902722707430257 ) ) ;
#4467=ORIENTED_EDGE ( 'NONE', *, *, #6484, .F. ) ;
#4470=CARTESIAN_POINT ( 'NONE',  ( -0.5984201754795734907, -8.314755988442763979, -0.7022220667781372549 ) ) ;
#4516=CARTESIAN_POINT ( 'NONE',  ( 7.777900015783946408, 4.169681370001526055, -7.928862157988300297 ) ) ;
#4529=DIRECTION ( 'NONE',  ( -1.000000000000000000, 0.000000000000000000, 0.000000000000000000 ) ) ;
#4572=VECTOR ( 'NONE', #8993, 1000.000000000000000 ) ;
#4607=EDGE_CURVE ( 'NONE', #5261, #21434, #9318, .T. ) ;
#4608=DIRECTION ( 'NONE',  ( 0.5000000000000005551, -0.8660254037844383745, 0.000000000000000000 ) ) ;
#4633=VERTEX_POINT ( 'NONE', #9388 ) ;
#4731=EDGE_CURVE ( 'NONE', #29479, #22574, #30586, .T. ) ;
#4733=CARTESIAN_POINT ( 'NONE',  ( 4.250000000000000000, 0.000000000000000000, -9.449444346342714240 ) ) ;
#4743=AXIS2_PLACEMENT_3D ( 'NONE', #26593, #31713, #31873 ) ;
#4753=ORIENTED_EDGE ( 'NONE', *, *, #9929, .F. ) ;
#4760=ORIENTED_EDGE ( 'NONE', *, *, #23511, .T. ) ;
#4770=ORIENTED_EDGE ( 'NONE', *, *, #22643, .F. ) ;
#4807=VECTOR ( 'NONE', #12580, 1000.000000000000000 ) ;
#4823=EDGE_CURVE ( 'NONE', #31786, #29479, #20632, .T. ) ;
#4825=CONICAL_SURFACE ( 'NONE', #23862, 7.500000000000001776, 0.8594454914424796144 ) ;
#4864=CARTESIAN_POINT ( 'NONE',  ( -1.994931997373328159E-14, -8.660254037844390851, -1.000000000000000888 ) ) ;
#4870=CARTESIAN_POINT ( 'NONE',  ( -3.750000000000001776, 6.495190528383289141, -6.991905250253753756 ) ) ;
#4900=CARTESIAN_POINT ( 'NONE',  ( -7.500000000000000000, 3.202583086485915942, -7.213046687579523386 ) ) ;
#4908=DIRECTION ( 'NONE',  ( 0.000000000000000000, 0.000000000000000000, -1.000000000000000000 ) ) ;
#4961=CYLINDRICAL_SURFACE ( 'NONE', #17838, 4.250000000000000000 ) ;
#4969=ORIENTED_EDGE ( 'NONE', *, *, #23752, .T. ) ;
#4976=B_SPLINE_CURVE_WITH_KNOTS ( 'NONE', 3,
 ( #3844, #13037, #30938, #20873, #25820, #4864 ),
 .UNSPECIFIED., .F., .F.,
 ( 4, 2, 4 ),
 ( 0.004444412883774326306, 0.006655097293744431999, 0.008865781703714537693 ),
 .UNSPECIFIED. ) ;
#5024=ORIENTED_EDGE ( 'NONE', *, *, #8078, .F. ) ;
#5065=CARTESIAN_POINT ( 'NONE',  ( 0.000000000000000000, 0.000000000000000000, -9.974600000000000577 ) ) ;
#5068=CARTESIAN_POINT ( 'NONE',  ( -7.500000000000000000, -3.160302461882432024, -7.231849989190475725 ) ) ;
#5100=ORIENTED_EDGE ( 'NONE', *, *, #30794, .F. ) ;
#5105=DIRECTION ( 'NONE',  ( 0.000000000000000000, 0.000000000000000000, 1.000000000000000000 ) ) ;
#5115=FACE_OUTER_BOUND ( 'NONE', #22282, .T. ) ;
#5122=AXIS2_PLACEMENT_3D ( 'NONE', #8421, #23919, #21195 ) ;
#5132=CARTESIAN_POINT ( 'NONE',  ( 0.000000000000000000, 0.000000000000000000, -0.5251556536572846712 ) ) ;
#5134=MECHANICAL_DESIGN_GEOMETRIC_PRESENTATION_REPRESENTATION('',(#27423),#28537);
#5232=CARTESIAN_POINT ( 'NONE',  ( -7.499999999999999112, -4.652405105468739421, -7.929127756970856034 ) ) ;
#5261=VERTEX_POINT ( 'NONE', #8505 ) ;
#5288=DIRECTION ( 'NONE',  ( -0.8191520442889907994, 1.003171929053523514E-16, 0.5735764363510474917 ) ) ;
#5319=CARTESIAN_POINT ( 'NONE',  ( 7.499999999999999112, 2.575910028905302074, -0.3641256808890108720 ) ) ;
#5364=LINE ( 'NONE', #15250, #32274 ) ;
#5405=CARTESIAN_POINT ( 'NONE',  ( -7.500000000000000000, -3.948305025207388130, -7.349903712356284480 ) ) ;
#5450=CARTESIAN_POINT ( 'NONE',  ( -7.640563834021360018E-16, -9.147862274876560562, -8.047472243342937759 ) ) ;
#5461=DIRECTION ( 'NONE',  ( 0.000000000000000000, 0.000000000000000000, 1.000000000000000000 ) ) ;
#5621=CARTESIAN_POINT ( 'NONE',  ( 5.088535779737119569, -5.722386535631984295, -7.491772860715834703 ) ) ;
#5673=CARTESIAN_POINT ( 'NONE',  ( 0.04725809328185039127, -9.175759667312528123, -8.057670357645362103 ) ) ;
#5677=CARTESIAN_POINT ( 'NONE',  ( -7.907996613752304782, -3.055722423191990611, -7.792112796859422374 ) ) ;
#5688=CARTESIAN_POINT ( 'NONE',  ( -0.3483149870578547969, 8.861353789385022495, -7.493854785173811983 ) ) ;
#5776=CARTESIAN_POINT ( 'NONE',  ( 2.558993250143296372, -7.638875775590942219, -7.593821156097518177 ) ) ;
#5778=EDGE_CURVE ( 'NONE', #8601, #31418, #8571, .T. ) ;
#5948=CARTESIAN_POINT ( 'NONE',  ( 4.419133455864432847, -6.108866147516184952, -7.026396753507086146 ) ) ;
#6027=CONICAL_SURFACE ( 'NONE', #19101, 7.500000000000001776, 0.8594454914424796144 ) ;
#6065=CARTESIAN_POINT ( 'NONE',  ( 3.749999999999998224, 6.495190528383290918, -6.991905250253753756 ) ) ;
#6069=DIRECTION ( 'NONE',  ( 0.8191520442889907994, 1.003171929053523514E-16, -0.5735764363510474917 ) ) ;
#6078=CARTESIAN_POINT ( 'NONE',  ( 4.606548227981508425, 6.456511556909250160, -7.591235721156633254 ) ) ;
#6110=CARTESIAN_POINT ( 'NONE',  ( 1.249327701954825010, -8.410337540182549532, -7.776713651265369620 ) ) ;
#6129=ADVANCED_FACE ( 'NONE', ( #24588 ), #31476, .T. ) ;
#6149=DIRECTION ( 'NONE',  ( -0.000000000000000000, -0.000000000000000000, 1.000000000000000000 ) ) ;
#6167=CIRCLE ( 'NONE', #12722, 5.000000000000001776 ) ;
#6169=VECTOR ( 'NONE', #6516, 1000.000000000000000 ) ;
#6170=CARTESIAN_POINT ( 'NONE',  ( -3.080866544137490504, -6.881514909249304424, -7.026396753507435200 ) ) ;
#6171=ORIENTED_EDGE ( 'NONE', *, *, #31618, .F. ) ;
#6240=CYLINDRICAL_SURFACE ( 'NONE', #467, 4.250000000000000000 ) ;
#6244=CARTESIAN_POINT ( 'NONE',  ( 7.500000000000000000, -3.202733125947433201, -7.213074474936314928 ) ) ;
#6257=ORIENTED_EDGE ( 'NONE', *, *, #29497, .T. ) ;
#6313=DIRECTION ( 'NONE',  ( 1.224646799147353207E-16, 1.000000000000000000, 0.000000000000000000 ) ) ;
#6342=VERTEX_POINT ( 'NONE', #18449 ) ;
#6364=DIRECTION ( 'NONE',  ( 0.000000000000000000, 0.000000000000000000, -1.000000000000000000 ) ) ;
#6432=CARTESIAN_POINT ( 'NONE',  ( 2.621086668468698644, 7.606368536631364030, -7.634085501268425666 ) ) ;
#6442=DIRECTION ( 'NONE',  ( -0.9396926207859143121, 0.000000000000000000, -0.3420201433256525592 ) ) ;
#6454=CARTESIAN_POINT ( 'NONE',  ( -7.025762299539908296E-16, -8.895730773063899477, -7.917997657324741034 ) ) ;
#6476=EDGE_CURVE ( 'NONE', #7575, #12674, #23239, .T. ) ;
#6484=EDGE_CURVE ( 'NONE', #24452, #32263, #28903, .T. ) ;
#6512=CARTESIAN_POINT ( 'NONE',  ( -5.276765049035075705, 6.073111908730296271, -7.634085501268424778 ) ) ;
#6516=DIRECTION ( 'NONE',  ( 0.000000000000000000, 0.000000000000000000, 1.000000000000000000 ) ) ;
#6573=AXIS2_PLACEMENT_3D ( 'NONE', #13081, #4908, #2189 ) ;
#6595=ORIENTED_EDGE ( 'NONE', *, *, #18744, .F. ) ;
#6612=ADVANCED_FACE ( 'NONE', ( #13579 ), #6240, .F. ) ;
#6631=CARTESIAN_POINT ( 'NONE',  ( 7.500000000000000000, 4.330127018922199866, -1.000000000000000888 ) ) ;
#6712=CARTESIAN_POINT ( 'NONE',  ( -2.558993250147282073, 7.638875775587784744, -7.593821156097241065 ) ) ;
#6811=EDGE_CURVE ( 'NONE', #18459, #17539, #28054, .T. ) ;
#6835=CARTESIAN_POINT ( 'NONE',  ( 0.000000000000000000, 0.000000000000000000, -9.999999999999998224 ) ) ;
#6858=EDGE_CURVE ( 'NONE', #12674, #17539, #21956, .T. ) ;
#6868=EDGE_CURVE ( 'NONE', #16155, #2927, #11335, .T. ) ;
#6897=LINE ( 'NONE', #22742, #31182 ) ;
#6918=CARTESIAN_POINT ( 'NONE',  ( -7.703920929261752981, 4.447860822324863683, -7.917989418073281271 ) ) ;
#6931=AXIS2_PLACEMENT_3D ( 'NONE', #21773, #27057, #11065 ) ;
#6943=ORIENTED_EDGE ( 'NONE', *, *, #16321, .F. ) ;
#6967=DIRECTION ( 'NONE',  ( 0.000000000000000000, 0.000000000000000000, -1.000000000000000000 ) ) ;
#7015=CIRCLE ( 'NONE', #1562, 7.500000000000001776 ) ;
#7026=ORIENTED_EDGE ( 'NONE', *, *, #19384, .F. ) ;
#7036=CARTESIAN_POINT ( 'NONE',  ( -1.206569728928481577, -7.963640680051488729, -0.4524126574264552558 ) ) ;
#7071=EDGE_CURVE ( 'NONE', #854, #16934, #26084, .T. ) ;
#7086=( NAMED_UNIT ( * ) PLANE_ANGLE_UNIT ( ) SI_UNIT ( $, .RADIAN. ) );
#7185=CARTESIAN_POINT ( 'NONE',  ( -2.499999999999999556, -7.216878364870334295, -7.063244554130003294 ) ) ;
#7202=CARTESIAN_POINT ( 'NONE',  ( -7.500000000000001776, 0.000000000000000000, 0.000000000000000000 ) ) ;
#7219=DIRECTION ( 'NONE',  ( -0.8191520442889907994, 0.000000000000000000, -0.5735764363510474917 ) ) ;
#7237=CARTESIAN_POINT ( 'NONE',  ( -0.5974722283283655511, 8.315303285985683246, -0.7026937717022859742 ) ) ;
#7257=CARTESIAN_POINT ( 'NONE',  ( 0.000000000000000000, 0.000000000000000000, 0.000000000000000000 ) ) ;
#7264=CARTESIAN_POINT ( 'NONE',  ( -0.6250000000000001110, 8.299410119600874935, -7.298562697733108173 ) ) ;
#7299=CARTESIAN_POINT ( 'NONE',  ( -7.922811899608408481, -4.628803996615321381, -8.057669882367649805 ) ) ;
#7356=DIRECTION ( 'NONE',  ( -0.000000000000000000, -0.000000000000000000, 1.000000000000000000 ) ) ;
#7362=DIRECTION ( 'NONE',  ( 0.000000000000000000, 0.000000000000000000, -1.000000000000000000 ) ) ;
#7393=CARTESIAN_POINT ( 'NONE',  ( -1.015826369459165157, 8.073766409993364590, -7.642786413619490737 ) ) ;
#7468=DIRECTION ( 'NONE',  ( -0.000000000000000000, -0.000000000000000000, 1.000000000000000000 ) ) ;
#7548=EDGE_LOOP ( 'NONE', ( #19714, #12605, #14002, #22948 ) ) ;
#7575=VERTEX_POINT ( 'NONE', #28180 ) ;
#7605=CIRCLE ( 'NONE', #26105, 4.250000000000000000 ) ;
#7636=CARTESIAN_POINT ( 'NONE',  ( -7.500000000000000000, 4.730921838224027454, -7.493596905200499592 ) ) ;
#7640=CARTESIAN_POINT ( 'NONE',  ( 7.922281120364393914, -4.573931137438282057, -8.047472243342932430 ) ) ;
#7643=DIRECTION ( 'NONE',  ( -0.000000000000000000, -0.000000000000000000, 1.000000000000000000 ) ) ;
#7667=EDGE_LOOP ( 'NONE', ( #14684, #22306 ) ) ;
#7678=CARTESIAN_POINT ( 'NONE',  ( 5.047120108843200725, -5.746297884371399434, -0.1007566405101860824 ) ) ;
#7680=DIRECTION ( 'NONE',  ( 0.8660254037844381525, -0.5000000000000007772, 0.000000000000000000 ) ) ;
#7687=VECTOR ( 'NONE', #19891, 1000.000000000000000 ) ;
#7706=ORIENTED_EDGE ( 'NONE', *, *, #11621, .T. ) ;
#7712=ORIENTED_EDGE ( 'NONE', *, *, #8553, .T. ) ;
#7799=CARTESIAN_POINT ( 'NONE',  ( -7.894706624614703294, -0.7534108004380160040, -7.590222617908770175 ) ) ;
#7801=ORIENTED_EDGE ( 'NONE', *, *, #30794, .T. ) ;
#7861=CARTESIAN_POINT ( 'NONE',  ( 0.000000000000000000, 0.000000000000000000, -10.00000000000000000 ) ) ;
#7866=CARTESIAN_POINT ( 'NONE',  ( 7.500000000000000000, 4.330127018922190096, -10.00000000000000000 ) ) ;
#7885=EDGE_CURVE ( 'NONE', #21434, #6342, #22819, .T. ) ;
#7940=DIRECTION ( 'NONE',  ( 1.000000000000000000, 0.000000000000000000, 0.000000000000000000 ) ) ;
#7960=CARTESIAN_POINT ( 'NONE',  ( 2.818872373871549124E-16, 8.716839668575678601, -7.700121441565840996 ) ) ;
#7965=CARTESIAN_POINT ( 'NONE',  ( -3.750000000000007105, -6.495190528383289141, 0.000000000000000000 ) ) ;
#7968=CARTESIAN_POINT ( 'NONE',  ( -7.500000000000000000, -1.572902445675612659, -7.069816568113127531 ) ) ;
#7973=CLOSED_SHELL ( 'NONE', ( #3484, #25957, #2672, #18424, #3265, #6612, #28681, #17173, #8373, #10222, #435, #2538, #15019, #23489, #10262, #33684, #3305, #3700, #6129, #27391, #14810, #23421, #2254, #22405, #28711, #1208, #29491, #27695, #26811, #2909, #30948, #9322 ) ) ;
#7999=ORIENTED_EDGE ( 'NONE', *, *, #20345, .T. ) ;
#8018=DIRECTION ( 'NONE',  ( -0.000000000000000000, -0.000000000000000000, 1.000000000000000000 ) ) ;
#8050=ORIENTED_EDGE ( 'NONE', *, *, #27650, .T. ) ;
#8055=VERTEX_POINT ( 'NONE', #32727 ) ;
#8057=CARTESIAN_POINT ( 'NONE',  ( 7.500000000000002665, 3.988838049906435312, -0.8529248949437669980 ) ) ;
#8078=EDGE_CURVE ( 'NONE', #18459, #25811, #1360, .T. ) ;
#8096=ORIENTED_EDGE ( 'NONE', *, *, #2094, .T. ) ;
#8103=SURFACE_STYLE_USAGE ( .BOTH. , #10823 ) ;
#8155=FACE_OUTER_BOUND ( 'NONE', #26546, .T. ) ;
#8166=DIRECTION ( 'NONE',  ( 0.000000000000000000, 0.000000000000000000, 1.000000000000000000 ) ) ;
#8175=CARTESIAN_POINT ( 'NONE',  ( 7.922281120364393914, 4.573931137438269623, -8.047472243342930653 ) ) ;
#8237=CARTESIAN_POINT ( 'NONE',  ( 4.999999999999999112, -5.773502691896267081, -7.063244554130005071 ) ) ;
#8240=AXIS2_PLACEMENT_3D ( 'NONE', #30806, #7468, #17852 ) ;
#8289=EDGE_CURVE ( 'NONE', #12471, #31786, #7605, .T. ) ;
#8311=CARTESIAN_POINT ( 'NONE',  ( 7.500000000000000000, -1.645076096015019695, -7.030022527230891605 ) ) ;
#8341=CARTESIAN_POINT ( 'NONE',  ( -7.640563834021360018E-16, -9.147862274876560562, -8.047472243342937759 ) ) ;
#8351=FILL_AREA_STYLE ('',( #32175 ) ) ;
#8373=ADVANCED_FACE ( 'NONE', ( #25743 ), #30519, .T. ) ;
#8404=CARTESIAN_POINT ( 'NONE',  ( -5.335963852939856089, -6.035591050534137025, -7.593821156097342318 ) ) ;
#8413=CARTESIAN_POINT ( 'NONE',  ( 0.000000000000000000, 0.000000000000000000, -9.974600000000000577 ) ) ;
#8417=CARTESIAN_POINT ( 'NONE',  ( 7.499999999999999112, -4.330127018922205195, -1.000000000000000888 ) ) ;
#8421=CARTESIAN_POINT ( 'NONE',  ( 0.000000000000000000, 0.000000000000000000, -9.226681596905677907 ) ) ;
#8482=ORIENTED_EDGE ( 'NONE', *, *, #33140, .F. ) ;
#8500=CARTESIAN_POINT ( 'NONE',  ( -7.640563834021360018E-16, -9.147862274876560562, -8.047472243342937759 ) ) ;
#8505=CARTESIAN_POINT ( 'NONE',  ( -3.750000000000004885, 6.495190528383289141, 0.000000000000000000 ) ) ;
#8553=EDGE_CURVE ( 'NONE', #17539, #1999, #24957, .T. ) ;
#8571=B_SPLINE_CURVE_WITH_KNOTS ( 'NONE', 3,
 ( #8417, #23748, #28862, #13522, #13191, #746, #26633, #18307 ),
 .UNSPECIFIED., .F., .F.,
 ( 4, 2, 2, 4 ),
 ( 0.006061689441712453386, 0.007174127271521678166, 0.008286565101330902947, 0.01051144076094935251 ),
 .UNSPECIFIED. ) ;
#8601=VERTEX_POINT ( 'NONE', #16019 ) ;
#8710=CARTESIAN_POINT ( 'NONE',  ( 7.549006887134069643, 4.358421158401191597, -7.700127545397312367 ) ) ;
#8835=SURFACE_STYLE_FILL_AREA ( #8351 ) ;
#8843=CARTESIAN_POINT ( 'NONE',  ( -7.500000000000000000, -2.571118828324945760, -0.3627527587569098766 ) ) ;
#8872=CARTESIAN_POINT ( 'NONE',  ( 0.000000000000000000, 0.000000000000000000, 0.000000000000000000 ) ) ;
#8873=CARTESIAN_POINT ( 'NONE',  ( -10.12668159690567649, 1.240160820363494356E-15, -9.226681596905677907 ) ) ;
#8916=B_SPLINE_CURVE_WITH_KNOTS ( 'NONE', 3,
 ( #20772, #31505, #31168, #13107, #28615, #23166 ),
 .UNSPECIFIED., .F., .F.,
 ( 4, 2, 4 ),
 ( 0.004615310220740751271, 0.006918661718823357169, 0.009222013216905963068 ),
 .UNSPECIFIED. ) ;
#8948=DIRECTION ( 'NONE',  ( 0.000000000000000000, 0.000000000000000000, -1.000000000000000000 ) ) ;
#8993=DIRECTION ( 'NONE',  ( -0.000000000000000000, -0.000000000000000000, 1.000000000000000000 ) ) ;
#8998=ORIENTED_EDGE ( 'NONE', *, *, #2109, .T. ) ;
#9064=ORIENTED_EDGE ( 'NONE', *, *, #12679, .F. ) ;
#9294=CONICAL_SURFACE ( 'NONE', #6573, 10.39117206796836079, 1.221730476396047926 ) ;
#9318=CIRCLE ( 'NONE', #3335, 7.500000000000001776 ) ;
#9322=ADVANCED_FACE ( 'NONE', ( #16204 ), #3592, .F. ) ;
#9325=CARTESIAN_POINT ( 'NONE',  ( -6.127431526422343306E-17, 9.147862274876549904, -8.047472243342932430 ) ) ;
#9331=FACE_OUTER_BOUND ( 'NONE', #7667, .T. ) ;
#9388=CARTESIAN_POINT ( 'NONE',  ( 3.750000000000004441, -6.495190528383289141, 0.000000000000000000 ) ) ;
#9395=PRODUCT_DEFINITION_FORMATION_WITH_SPECIFIED_SOURCE ( 'ANY', '', #22203, .NOT_KNOWN. ) ;
#9413=ORIENTED_EDGE ( 'NONE', *, *, #2302, .F. ) ;
#9433=CARTESIAN_POINT ( 'NONE',  ( -7.779103221381273414, 4.168986698926021361, -7.929128246061903695 ) ) ;
#9534=EDGE_CURVE ( 'NONE', #7575, #613, #3336, .T. ) ;
#9568=DIRECTION ( 'NONE',  ( 0.000000000000000000, 0.000000000000000000, 1.000000000000000000 ) ) ;
#9705=AXIS2_PLACEMENT_3D ( 'NONE', #9991, #12705, #25993 ) ;
#9747=AXIS2_PLACEMENT_3D ( 'NONE', #15340, #8018, #2571 ) ;
#9769=DIRECTION ( 'NONE',  ( -1.000000000000000000, 0.000000000000000000, 0.000000000000000000 ) ) ;
#9776=CARTESIAN_POINT ( 'NONE',  ( -5.276498195231978272, 6.073236878017963747, -7.633618187056680604 ) ) ;
#9794=CARTESIAN_POINT ( 'NONE',  ( -3.096526599377909417, 6.872473572140716414, 1.143494478793305063E-15 ) ) ;
#9814=( NAMED_UNIT ( * ) SI_UNIT ( $, .STERADIAN. ) SOLID_ANGLE_UNIT ( ) );
#9905=CARTESIAN_POINT ( 'NONE',  ( 0.000000000000000000, 0.000000000000000000, 0.000000000000000000 ) ) ;
#9911=DIRECTION ( 'NONE',  ( 1.000000000000000000, 0.000000000000000000, 0.000000000000000000 ) ) ;
#9929=EDGE_CURVE ( 'NONE', #8601, #4633, #30566, .T. ) ;
#9979=AXIS2_PLACEMENT_3D ( 'NONE', #16779, #8948, #24453 ) ;
#9991=CARTESIAN_POINT ( 'NONE',  ( 0.000000000000000000, 0.000000000000000000, -9.449444346342714240 ) ) ;
#10132=ORIENTED_EDGE ( 'NONE', *, *, #6484, .T. ) ;
#10165=B_SPLINE_CURVE_WITH_KNOTS ( 'NONE', 3,
 ( #26134, #13511, #5677, #3795, #26621, #29356 ),
 .UNSPECIFIED., .F., .F.,
 ( 4, 2, 4 ),
 ( 0.000000000000000000, 0.002307655110370376069, 0.004615310220740751271 ),
 .UNSPECIFIED. ) ;
#10167=CONICAL_SURFACE ( 'NONE', #1448, 5.000000000000001776, 0.9599310885968795892 ) ;
#10189=CARTESIAN_POINT ( 'NONE',  ( -7.500000000000000000, -4.330127018922199866, -1.000000000000000888 ) ) ;
#10192=DIRECTION ( 'NONE',  ( -1.000000000000000000, 0.000000000000000000, 0.000000000000000000 ) ) ;
#10222=ADVANCED_FACE ( 'NONE', ( #662 ), #13435, .F. ) ;
#10225=DIRECTION ( 'NONE',  ( -1.000000000000000000, 0.000000000000000000, 0.000000000000000000 ) ) ;
#10244=CARTESIAN_POINT ( 'NONE',  ( 6.293430271071537518, -5.026740376715104652, -0.4524126574264552558 ) ) ;
#10262=ADVANCED_FACE ( 'NONE', ( #24838, #9331 ), #24674, .F. ) ;
#10331=DIRECTION ( 'NONE',  ( -0.000000000000000000, -0.000000000000000000, 1.000000000000000000 ) ) ;
#10364=CARTESIAN_POINT ( 'NONE',  ( -7.499999999999653610, -1.545780083834116247, -7.491787297939224821 ) ) ;
#10397=ORIENTED_EDGE ( 'NONE', *, *, #26748, .F. ) ;
#10460=( BOUNDED_SURFACE ( )  B_SPLINE_SURFACE ( 3, 2, ( 
 ( #10706, #26862, #18858 ),
 ( #6244, #29254, #16301 ),
 ( #8311, #3521, #16130 ),
 ( #18538, #16632, #26522 ),
 ( #21084, #10875, #3194 ),
 ( #11368, #13914, #478 ),
 ( #967, #21250, #13583 ),
 ( #24299, #21747, #19196 ) ),
 .UNSPECIFIED., .F., .F., .T. ) 
 B_SPLINE_SURFACE_WITH_KNOTS ( ( 4, 2, 2, 4 ),
 ( 3, 3 ),
 ( 0.03850042371095789562, 0.04313406099830585649, 0.04545087964197984387, 0.04776769828565382431 ),
 ( 0.000000000000000000, 1.000000000000000000 ),
 .UNSPECIFIED. ) 
 GEOMETRIC_REPRESENTATION_ITEM ( )  RATIONAL_B_SPLINE_SURFACE ( (
 ( 1.000000000000000000, 0.8047781847388135734, 1.000000000000000000),
 ( 1.000000000000000000, 0.8123760230793541925, 1.000000000000000000),
 ( 1.000000000000000000, 0.8190653851695529619, 1.000000000000000000),
 ( 1.000000000000000000, 0.8191940386278896424, 1.000000000000000000),
 ( 1.000000000000000000, 0.8176096570055705337, 1.000000000000000000),
 ( 1.000000000000000000, 0.8122964723277524834, 1.000000000000000000),
 ( 1.000000000000000000, 0.8086312464132844324, 1.000000000000000000),
 ( 1.000000000000000000, 0.8047712192439641088, 1.000000000000000000) ) ) 
 REPRESENTATION_ITEM ( '' )  SURFACE ( )  );
#10488=CARTESIAN_POINT ( 'NONE',  ( 2.411464220263165092, 7.267994521134541586, -7.491772860716163329 ) ) ;
#10522=CARTESIAN_POINT ( 'NONE',  ( 2.547548355748054857E-16, 8.895721644649732696, -7.917989418073286600 ) ) ;
#10530=CARTESIAN_POINT ( 'NONE',  ( -7.908228835406498902, 3.123118350879302341, -7.776694659841278501 ) ) ;
#10595=CIRCLE ( 'NONE', #14923, 4.250000000000000000 ) ;
#10652=CARTESIAN_POINT ( 'NONE',  ( 5.174575781541291164, 5.672711317429402378, -7.030005583190089169 ) ) ;
#10685=UNCERTAINTY_MEASURE_WITH_UNIT (LENGTH_MEASURE( 1.000000000000000082E-05 ), #29632, 'distance_accuracy_value', 'NONE');
#10706=CARTESIAN_POINT ( 'NONE',  ( 7.500000000000000000, -4.730916290271713898, -7.493595886788494198 ) ) ;
#10720=EDGE_LOOP ( 'NONE', ( #10764, #7712, #26502, #30891, #16944 ) ) ;
#10753=LINE ( 'NONE', #23369, #20074 ) ;
#10764=ORIENTED_EDGE ( 'NONE', *, *, #30412, .F. ) ;
#10801=CARTESIAN_POINT ( 'NONE',  ( -0.3875187462251565851, -8.436519985395204202, -7.781689322724289148 ) ) ;
#10819=AXIS2_PLACEMENT_3D ( 'NONE', #8873, #6313, #21653 ) ;
#10823=SURFACE_SIDE_STYLE ('',( #31274 ) ) ;
#10875=CARTESIAN_POINT ( 'NONE',  ( 7.500000000000000000, 1.545478204151513157, -7.491761935628701075 ) ) ;
#10913=CARTESIAN_POINT ( 'NONE',  ( 6.439685834477092641, -4.942299687812566233, -7.659344964963564983 ) ) ;
#10967=ORIENTED_EDGE ( 'NONE', *, *, #17958, .F. ) ;
#11035=LINE ( 'NONE', #31488, #3728 ) ;
#11065=DIRECTION ( 'NONE',  ( 0.000000000000000000, 0.000000000000000000, 1.000000000000000000 ) ) ;
#11070=CARTESIAN_POINT ( 'NONE',  ( 1.305263714129178743, -8.377797850839291627, -7.792447862505339273 ) ) ;
#11101=ORIENTED_EDGE ( 'NONE', *, *, #8289, .T. ) ;
#11120=CARTESIAN_POINT ( 'NONE',  ( -7.922281120364393914, -4.573931137438277617, -8.047472243342932430 ) ) ;
#11133=CARTESIAN_POINT ( 'NONE',  ( 1.249999999999999112, -7.938566201357367902, -7.198902722707431145 ) ) ;
#11170=FACE_OUTER_BOUND ( 'NONE', #30022, .T. ) ;
#11173=ORIENTED_EDGE ( 'NONE', *, *, #1797, .T. ) ;
#11220=ORIENTED_EDGE ( 'NONE', *, *, #12277, .T. ) ;
#11335=CIRCLE ( 'NONE', #9705, 4.250000000000000000 ) ;
#11359=CIRCLE ( 'NONE', #30414, 7.500000000000001776 ) ;
#11363=CARTESIAN_POINT ( 'NONE',  ( 6.874999999999999112, 4.690970937165706900, -7.298562697733104621 ) ) ;
#11368=CARTESIAN_POINT ( 'NONE',  ( 7.500000000000000000, 3.160172554975063886, -7.231829826456836585 ) ) ;
#11390=CARTESIAN_POINT ( 'NONE',  ( 5.000000000000000888, 0.000000000000000000, -25.03750572909317285 ) ) ;
#11410=CARTESIAN_POINT ( 'NONE',  ( 0.9763930676190096802, -8.096533237419681228, -7.213065638943101376 ) ) ;
#11428=CARTESIAN_POINT ( 'NONE',  ( 7.500000000000000000, -4.330127018922199866, -7.422398894150035176 ) ) ;
#11460=CARTESIAN_POINT ( 'NONE',  ( 7.500000000000000000, -4.330127018922199866, -7.422398894150035176 ) ) ;
#11468=UNCERTAINTY_MEASURE_WITH_UNIT (LENGTH_MEASURE( 1.000000000000000082E-05 ), #13039, 'distance_accuracy_value', 'NONE');
#11526=DIRECTION ( 'NONE',  ( 0.000000000000000000, 0.000000000000000000, 1.000000000000000000 ) ) ;
#11540=CARTESIAN_POINT ( 'NONE',  ( 1.306442393143578906, 8.377108146505383601, -7.792327460285857654 ) ) ;
#11562=EDGE_CURVE ( 'NONE', #24712, #7575, #12971, .T. ) ;
#11614=( GEOMETRIC_REPRESENTATION_CONTEXT ( 3 ) GLOBAL_UNCERTAINTY_ASSIGNED_CONTEXT ( ( #19636 ) ) GLOBAL_UNIT_ASSIGNED_CONTEXT ( ( #22758, #7086, #9814 ) ) REPRESENTATION_CONTEXT ( 'NONE', 'WORKASPACE' ) );
#11621=EDGE_CURVE ( 'NONE', #14265, #33504, #28487, .T. ) ;
#11623=CARTESIAN_POINT ( 'NONE',  ( -2.623433461001184686, 7.604994000793856124, -7.633824513837113912 ) ) ;
#11683=EDGE_LOOP ( 'NONE', ( #6257, #15909, #33420, #27256, #3704, #28135, #4969 ) ) ;
#11685=EDGE_LOOP ( 'NONE', ( #7801, #21064, #7706, #12262 ) ) ;
#11721=CARTESIAN_POINT ( 'NONE',  ( -5.000000000000000888, 6.123233995736767268E-16, -10.00000000000000000 ) ) ;
#11725=DIRECTION ( 'NONE',  ( 0.000000000000000000, 0.000000000000000000, 1.000000000000000000 ) ) ;
#11897=VERTEX_POINT ( 'NONE', #5450 ) ;
#11935=FACE_OUTER_BOUND ( 'NONE', #27046, .T. ) ;
#11941=DIRECTION ( 'NONE',  ( 0.000000000000000000, 0.000000000000000000, 1.000000000000000000 ) ) ;
#11968=CARTESIAN_POINT ( 'NONE',  ( 7.500000000000000000, 4.330127018922199866, -1.000000000000000888 ) ) ;
#11980=DIRECTION ( 'NONE',  ( -0.000000000000000000, -0.000000000000000000, -1.000000000000000000 ) ) ;
#12007=ORIENTED_EDGE ( 'NONE', *, *, #6868, .T. ) ;
#12016=CARTESIAN_POINT ( 'NONE',  ( -7.500000000000000888, 2.575910028905295857, -0.3641256808890092067 ) ) ;
#12049=EDGE_CURVE ( 'NONE', #948, #11897, #18218, .T. ) ;
#12056=ORIENTED_EDGE ( 'NONE', *, *, #2470, .F. ) ;
#12088=CARTESIAN_POINT ( 'NONE',  ( -7.894787914004607998, -1.230850257101226302E-13, -7.591390474663425536 ) ) ;
#12117=CARTESIAN_POINT ( 'NONE',  ( 0.000000000000000000, 0.000000000000000000, 0.000000000000000000 ) ) ;
#12260=CARTESIAN_POINT ( 'NONE',  ( -7.500000000000000000, 4.330127018922191873, -0.9999999999999970024 ) ) ;
#12262=ORIENTED_EDGE ( 'NONE', *, *, #20440, .F. ) ;
#12277=EDGE_CURVE ( 'NONE', #12741, #1999, #33658, .T. ) ;
#12290=CARTESIAN_POINT ( 'NONE',  ( -5.000000000000000000, -5.773502691896264416, -7.063244554130003294 ) ) ;
#12317=CARTESIAN_POINT ( 'NONE',  ( 0.000000000000000000, 0.000000000000000000, -9.974600000000000577 ) ) ;
#12326=CARTESIAN_POINT ( 'NONE',  ( -7.500000000000000000, -4.330127018922199866, -1.000000000000000888 ) ) ;
#12391=( BOUNDED_SURFACE ( )  B_SPLINE_SURFACE ( 3, 2, ( 
 ( #14009, #12884, #24407 ),
 ( #13507, #24062, #21336 ),
 ( #29513, #32071, #8404 ),
 ( #6170, #31733, #23277 ),
 ( #13842, #566, #26955 ),
 ( #29352, #19291, #25838 ),
 ( #23901, #10801, #18791 ),
 ( #16561, #21175, #5673 ) ),
 .UNSPECIFIED., .F., .F., .T. ) 
 B_SPLINE_SURFACE_WITH_KNOTS ( ( 4, 2, 2, 4 ),
 ( 3, 3 ),
 ( 0.03861844051980971304, 0.04325213341840642572, 0.04556897986770477860, 0.04788582631700313841 ),
 ( 0.000000000000000000, 1.000000000000000000 ),
 .UNSPECIFIED. ) 
 GEOMETRIC_REPRESENTATION_ITEM ( )  RATIONAL_B_SPLINE_SURFACE ( (
 ( 1.000000000000000000, 0.8047781759831923454, 1.000000000000000000),
 ( 1.000000000000000000, 0.8123762462805160789, 1.000000000000000000),
 ( 1.000000000000000000, 0.8190659850616602844, 1.000000000000000000),
 ( 1.000000000000000000, 0.8191937571013702124, 1.000000000000000000),
 ( 1.000000000000000000, 0.8176092952780309453, 1.000000000000000000),
 ( 1.000000000000000000, 0.8122962088596628050, 1.000000000000000000),
 ( 1.000000000000000000, 0.8086311330827828936, 1.000000000000000000),
 ( 1.000000000000000000, 0.8047712282214327661, 1.000000000000000000) ) ) 
 REPRESENTATION_ITEM ( '' )  SURFACE ( )  );
#12471=VERTEX_POINT ( 'NONE', #17561 ) ;
#12479=EDGE_LOOP ( 'NONE', ( #15740, #31368, #13523, #32373 ) ) ;
#12524=EDGE_CURVE ( 'NONE', #3624, #2685, #27986, .T. ) ;
#12580=DIRECTION ( 'NONE',  ( 0.000000000000000000, 0.000000000000000000, 1.000000000000000000 ) ) ;
#12594=ORIENTED_EDGE ( 'NONE', *, *, #33019, .F. ) ;
#12605=ORIENTED_EDGE ( 'NONE', *, *, #29322, .T. ) ;
#12618=CARTESIAN_POINT ( 'NONE',  ( -7.500000000000000000, 4.330127018922191873, -0.9999999999999970024 ) ) ;
#12621=FACE_OUTER_BOUND ( 'NONE', #12479, .T. ) ;
#12674=VERTEX_POINT ( 'NONE', #31032 ) ;
#12679=EDGE_CURVE ( 'NONE', #25041, #5261, #3958, .T. ) ;
#12705=DIRECTION ( 'NONE',  ( -0.000000000000000000, -0.000000000000000000, 1.000000000000000000 ) ) ;
#12722=AXIS2_PLACEMENT_3D ( 'NONE', #8413, #25968, #2971 ) ;
#12730=MANIFOLD_SOLID_BREP ( 'EndChamfer', #7973 ) ;
#12739=CARTESIAN_POINT ( 'NONE',  ( -7.500000000000000000, 1.644753667986373458, -7.029983668655349405 ) ) ;
#12741=VERTEX_POINT ( 'NONE', #24011 ) ;
#12745=CARTESIAN_POINT ( 'NONE',  ( 7.894787914004607998, -0.7647108141804126458, -7.591390474663421095 ) ) ;
#12821=CARTESIAN_POINT ( 'NONE',  ( 7.499999999999999112, 0.7513028741560161539, -0.02472015219302839059 ) ) ;
#12884=CARTESIAN_POINT ( 'NONE',  ( -7.777900015783941967, -4.169681370001537601, -7.928862157988302073 ) ) ;
#12903=CARTESIAN_POINT ( 'NONE',  ( -7.500000000000698996, 1.613867362005801054, -7.450195926347907616 ) ) ;
#12905=ORIENTED_EDGE ( 'NONE', *, *, #6476, .T. ) ;
#12955=CARTESIAN_POINT ( 'NONE',  ( -7.640563834021360018E-16, -9.147862274876560562, -8.047472243342937759 ) ) ;
#12971=B_SPLINE_CURVE_WITH_KNOTS ( 'NONE', 3,
 ( #24216, #1212, #16879, #21997, #13652, #879, #27274, #1053, #29160 ),
 .UNSPECIFIED., .F., .F.,
 ( 4, 2, 1, 2, 4 ),
 ( 0.000000000000000000, 0.002165063509461097498, 0.004330127018922194995, 0.006495190528383292493, 0.008660254037844389990 ),
 .UNSPECIFIED. ) ;
#13029=EDGE_LOOP ( 'NONE', ( #4012, #12056, #13560, #33034 ) ) ;
#13033=CARTESIAN_POINT ( 'NONE',  ( 6.658902113225075858, 5.287118297641098863, -7.776713651267108673 ) ) ;
#13037=CARTESIAN_POINT ( 'NONE',  ( 3.096526599377912525, -6.872473572140722631, -5.976664475826341615E-15 ) ) ;
#13038=EDGE_CURVE ( 'NONE', #31786, #12471, #10595, .T. ) ;
#13039=( LENGTH_UNIT ( ) NAMED_UNIT ( * ) SI_UNIT ( .MILLI., .METRE. ) );
#13069=DIRECTION ( 'NONE',  ( -1.000000000000000000, 0.000000000000000000, 0.000000000000000000 ) ) ;
#13081=CARTESIAN_POINT ( 'NONE',  ( 0.000000000000000000, 0.000000000000000000, -8.499999999999998224 ) ) ;
#13107=CARTESIAN_POINT ( 'NONE',  ( -7.908030677224553884, 3.059924800338342799, -7.792662696733364314 ) ) ;
#13128=DIRECTION ( 'NONE',  ( 1.000000000000000000, 0.000000000000000000, 0.000000000000000000 ) ) ;
#13134=CARTESIAN_POINT ( 'NONE',  ( -7.500000000000000888, -1.443375672974068769, -7.063244554130002406 ) ) ;
#13135=DIRECTION ( 'NONE',  ( 0.000000000000000000, 0.000000000000000000, 1.000000000000000000 ) ) ;
#13155=EDGE_LOOP ( 'NONE', ( #12007, #17114, #24487, #27790 ) ) ;
#13157=CARTESIAN_POINT ( 'NONE',  ( -5.000000000000001776, 0.000000000000000000, -9.974600000000000577 ) ) ;
#13191=CARTESIAN_POINT ( 'NONE',  ( 7.500000000000000000, -2.571118828324946648, -0.3627527587569098766 ) ) ;
#13193=CARTESIAN_POINT ( 'NONE',  ( 0.3875187462248268488, 8.436519985393664101, -7.781689322726965230 ) ) ;
#13235=CARTESIAN_POINT ( 'NONE',  ( 0.000000000000000000, 0.000000000000000000, -9.449444346342714240 ) ) ;
#13262=CARTESIAN_POINT ( 'NONE',  ( 10.12668159690567649, 0.000000000000000000, -9.226681596905677907 ) ) ;
#13279=CARTESIAN_POINT ( 'NONE',  ( -4.606548227981510202, -6.456511556909259930, -7.591235721156638583 ) ) ;
#13435=PLANE ( 'NONE',  #6931 ) ;
#13438=PLANE ( 'NONE',  #24980 ) ;
#13453=CARTESIAN_POINT ( 'NONE',  ( 7.298354728637812983, -4.926141412639873707, -7.913704048099693189 ) ) ;
#13468=ORIENTED_EDGE ( 'NONE', *, *, #33450, .T. ) ;
#13507=CARTESIAN_POINT ( 'NONE',  ( -6.523606932383669843, -4.893847819345372940, -7.213065638944913260 ) ) ;
#13511=CARTESIAN_POINT ( 'NONE',  ( -7.914973979435149687, -3.817460047930451239, -7.907502498112421563 ) ) ;
#13522=CARTESIAN_POINT ( 'NONE',  ( 7.499999999999999112, -2.930060224340428565, -0.4701183149080248036 ) ) ;
#13523=ORIENTED_EDGE ( 'NONE', *, *, #32658, .T. ) ;
#13546=AXIS2_PLACEMENT_3D ( 'NONE', #17552, #2225, #17045 ) ;
#13560=ORIENTED_EDGE ( 'NONE', *, *, #2883, .F. ) ;
#13579=FACE_OUTER_BOUND ( 'NONE', #7548, .T. ) ;
#13583=CARTESIAN_POINT ( 'NONE',  ( 7.915340744421234476, 3.857466640755322640, -7.913699667209310284 ) ) ;
#13652=CARTESIAN_POINT ( 'NONE',  ( 7.500000000000000000, -5.637851296924623057E-15, -6.991905250253753756 ) ) ;
#13681=CARTESIAN_POINT ( 'NONE',  ( 1.282512619718868541, 8.391164935524033197, -7.795653906408837486 ) ) ;
#13729=B_SPLINE_CURVE_WITH_KNOTS ( 'NONE', 3,
 ( #17248, #4470, #7036, #19972, #1921, #27636 ),
 .UNSPECIFIED., .F., .F.,
 ( 4, 2, 4 ),
 ( 2.475503369438313607E-07, 0.002222330217055647119, 0.004444412883774350592 ),
 .UNSPECIFIED. ) ;
#13738=CARTESIAN_POINT ( 'NONE',  ( 4.336808689942017736E-16, 8.660254037844390851, -1.000000000000000888 ) ) ;
#13742=CARTESIAN_POINT ( 'NONE',  ( 7.907996613752301229, 3.055722423191984838, -7.792112796859423263 ) ) ;
#13745=APPLICATION_CONTEXT ( 'automotive_design' ) ;
#13771=ORIENTED_EDGE ( 'NONE', *, *, #21349, .F. ) ;
#13778=CARTESIAN_POINT ( 'NONE',  ( 2.623433461001182909, -7.604994000793866782, -7.633824513837117465 ) ) ;
#13829=CARTESIAN_POINT ( 'NONE',  ( -7.808218555863076560, -4.508077085118260108, -7.999534413642739317 ) ) ;
#13842=CARTESIAN_POINT ( 'NONE',  ( -2.387978478801491278, -7.281554020289322970, -7.069802615102039667 ) ) ;
#13866=CARTESIAN_POINT ( 'NONE',  ( 0.000000000000000000, 0.000000000000000000, 0.000000000000000000 ) ) ;
#13914=CARTESIAN_POINT ( 'NONE',  ( 7.499999999999999112, 3.105728215500122680, -7.659336188854854122 ) ) ;
#13951=SURFACE_STYLE_USAGE ( .BOTH. , #19237 ) ;
#13984=CARTESIAN_POINT ( 'NONE',  ( 7.703928834700302986, -4.447865386531950627, -7.917997657324739258 ) ) ;
#14002=ORIENTED_EDGE ( 'NONE', *, *, #8289, .F. ) ;
#14009=CARTESIAN_POINT ( 'NONE',  ( -7.847095227763516867, -4.129731495738496960, -7.493596212620239783 ) ) ;
#14098=ORIENTED_EDGE ( 'NONE', *, *, #13038, .T. ) ;
#14102=LINE ( 'NONE', #11390, #4572 ) ;
#14159=CARTESIAN_POINT ( 'NONE',  ( 0.000000000000000000, 0.000000000000000000, -9.974600000000000577 ) ) ;
#14161=EDGE_CURVE ( 'NONE', #31418, #19301, #3469, .T. ) ;
#14198=DIRECTION ( 'NONE',  ( 1.000000000000000000, 0.000000000000000000, 0.000000000000000000 ) ) ;
#14265=VERTEX_POINT ( 'NONE', #13157 ) ;
#14333=CIRCLE ( 'NONE', #26299, 10.39117206796836079 ) ;
#14337=STYLED_ITEM ( 'NONE', ( #94 ), #26255 ) ;
#14425=( BOUNDED_SURFACE ( )  B_SPLINE_SURFACE ( 3, 2, ( 
 ( #7636, #17844, #18019 ),
 ( #4900, #23631, #10530 ),
 ( #12739, #12903, #31305 ),
 ( #28410, #23129, #7799 ),
 ( #7968, #10364, #28745 ),
 ( #5068, #20738, #15620 ),
 ( #5405, #31134, #15789 ),
 ( #18189, #5232, #7299 ) ),
 .UNSPECIFIED., .F., .F., .F. ) 
 B_SPLINE_SURFACE_WITH_KNOTS ( ( 4, 2, 2, 4 ),
 ( 3, 3 ),
 ( 0.03851319102641418551, 0.04314724750133520914, 0.04546427573879571749, 0.04778130397625623277 ),
 ( 0.000000000000000000, 1.000000000000000000 ),
 .UNSPECIFIED. ) 
 GEOMETRIC_REPRESENTATION_ITEM ( )  RATIONAL_B_SPLINE_SURFACE ( (
 ( 1.000000000000000000, 0.8047781573724569482, 1.000000000000000000),
 ( 1.000000000000000000, 0.8123768202405010630, 1.000000000000000000),
 ( 1.000000000000000000, 0.8190667609311549358, 1.000000000000000000),
 ( 1.000000000000000000, 0.8191933927154739781, 1.000000000000000000),
 ( 1.000000000000000000, 0.8176088169850088683, 1.000000000000000000),
 ( 1.000000000000000000, 0.8122958474542694152, 1.000000000000000000),
 ( 1.000000000000000000, 0.8086309703845098174, 1.000000000000000000),
 ( 1.000000000000000000, 0.8047712409910821041, 1.000000000000000000) ) ) 
 REPRESENTATION_ITEM ( '' )  SURFACE ( )  );
#14477=PLANE ( 'NONE',  #18872 ) ;
#14495=DIRECTION ( 'NONE',  ( 1.000000000000000000, 0.000000000000000000, 0.000000000000000000 ) ) ;
#14508=CARTESIAN_POINT ( 'NONE',  ( 5.000000000000000888, 0.000000000000000000, 0.000000000000000000 ) ) ;
#14538=CARTESIAN_POINT ( 'NONE',  ( -4.599534470795546781, 6.460478697738500031, -7.590212325761530821 ) ) ;
#14571=CARTESIAN_POINT ( 'NONE',  ( -7.500000000000001776, 0.000000000000000000, 0.000000000000000000 ) ) ;
#14599=EDGE_CURVE ( 'NONE', #24712, #948, #33171, .T. ) ;
#14639=ORIENTED_EDGE ( 'NONE', *, *, #4607, .F. ) ;
#14646=ORIENTED_EDGE ( 'NONE', *, *, #20300, .F. ) ;
#14681=B_SPLINE_CURVE_WITH_KNOTS ( 'NONE', 3,
 ( #21838, #16228, #11133, #31572, #3614, #8237, #18959, #26452, #11460 ),
 .UNSPECIFIED., .F., .F.,
 ( 4, 2, 1, 2, 4 ),
 ( 6.245710625686469831E-20, 0.002165063509461098365, 0.004330127018922195863, 0.006495190528383293360, 0.008660254037844389990 ),
 .UNSPECIFIED. ) ;
#14684=ORIENTED_EDGE ( 'NONE', *, *, #12524, .F. ) ;
#14720=AXIS2_PLACEMENT_3D ( 'NONE', #15506, #2566, #23350 ) ;
#14733=ORIENTED_EDGE ( 'NONE', *, *, #18880, .T. ) ;
#14796=CARTESIAN_POINT ( 'NONE',  ( 5.040301471719072168, 5.750234626350511746, -0.09933465333851003443 ) ) ;
#14810=ADVANCED_FACE ( 'NONE', ( #16294 ), #30052, .T. ) ;
#14848=CARTESIAN_POINT ( 'NONE',  ( 7.500000000000000000, 4.330127018922190096, -10.00000000000000000 ) ) ;
#14868=CARTESIAN_POINT ( 'NONE',  ( 10.39117206796836257, 0.000000000000000000, -8.499999999999998224 ) ) ;
#14878=CARTESIAN_POINT ( 'NONE',  ( -6.486836893983275232, 4.915077010913945443, -7.231838333420560261 ) ) ;
#14908=CARTESIAN_POINT ( 'NONE',  ( 7.968863443239234456, 4.547634245050474533, -8.057411785091787237 ) ) ;
#14923=AXIS2_PLACEMENT_3D ( 'NONE', #4404, #6967, #27907 ) ;
#15019=ADVANCED_FACE ( 'NONE', ( #4022 ), #1632, .T. ) ;
#15026=ORIENTED_EDGE ( 'NONE', *, *, #14599, .F. ) ;
#15047=CARTESIAN_POINT ( 'NONE',  ( -7.169303301815100227, 4.521054846639364300, -7.349897473154783256 ) ) ;
#15144=ORIENTED_EDGE ( 'NONE', *, *, #26748, .T. ) ;
#15153=ORIENTED_EDGE ( 'NONE', *, *, #20863, .F. ) ;
#15154=PRODUCT_DEFINITION_SHAPE ( 'NONE', 'NONE',  #27705 ) ;
#15168=DIRECTION ( 'NONE',  ( -1.000000000000000000, 0.000000000000000000, 0.000000000000000000 ) ) ;
#15209=CARTESIAN_POINT ( 'NONE',  ( 7.500000000000000000, 4.330127018922199866, -1.000000000000000888 ) ) ;
#15221=CARTESIAN_POINT ( 'NONE',  ( 0.3470952277635277472, 8.860649561028097310, -7.493596212620242447 ) ) ;
#15250=CARTESIAN_POINT ( 'NONE',  ( -5.007715329123872641E-16, -8.660254037844399733, -10.00000000000000000 ) ) ;
#15259=CONICAL_SURFACE ( 'NONE', #19614, 4.174999999999999822, 0.9599310885968795892 ) ;
#15284=CARTESIAN_POINT ( 'NONE',  ( -5.040301471719076609, -5.750234626350520628, -0.09933465333851741741 ) ) ;
#15333=B_SPLINE_CURVE_WITH_KNOTS ( 'NONE', 3,
 ( #16018, #18907, #16511, #350, #8843, #16342, #26736, #21130 ),
 .UNSPECIFIED., .F., .F.,
 ( 4, 2, 2, 4 ),
 ( 0.006061689441712453386, 0.007174127271521677299, 0.008286565101330901212, 0.01051144076094934904 ),
 .UNSPECIFIED. ) ;
#15340=CARTESIAN_POINT ( 'NONE',  ( 0.000000000000000000, 0.000000000000000000, -9.999999999999998224 ) ) ;
#15346=CARTESIAN_POINT ( 'NONE',  ( -4.174999999999999822, 5.112900386440199535E-16, -0.5776712190230133270 ) ) ;
#15446=CIRCLE ( 'NONE', #233, 7.500000000000001776 ) ;
#15472=FACE_OUTER_BOUND ( 'NONE', #28776, .T. ) ;
#15506=CARTESIAN_POINT ( 'NONE',  ( 0.000000000000000000, 0.000000000000000000, -0.5776712190230133270 ) ) ;
#15608=ORIENTED_EDGE ( 'NONE', *, *, #2109, .F. ) ;
#15620=CARTESIAN_POINT ( 'NONE',  ( -7.908219015560238319, -3.084967917785936820, -7.795665562178438535 ) ) ;
#15693=VECTOR ( 'NONE', #6442, 1000.000000000000000 ) ;
#15706=ORIENTED_EDGE ( 'NONE', *, *, #20345, .F. ) ;
#15740=ORIENTED_EDGE ( 'NONE', *, *, #29322, .F. ) ;
#15749=CARTESIAN_POINT ( 'NONE',  ( 2.387978478801324300, 7.281554020289410012, -7.069802615102035226 ) ) ;
#15789=CARTESIAN_POINT ( 'NONE',  ( -7.915341292092594294, -3.857523022641989652, -7.913710289178173873 ) ) ;
#15816=PLANE ( 'NONE',  #2572 ) ;
#15822=EDGE_LOOP ( 'NONE', ( #6595, #25072, #24540, #2806, #28876 ) ) ;
#15901=ORIENTED_EDGE ( 'NONE', *, *, #12679, .T. ) ;
#15909=ORIENTED_EDGE ( 'NONE', *, *, #3133, .T. ) ;
#15985=DIRECTION ( 'NONE',  ( 0.000000000000000000, -1.000000000000000000, 0.000000000000000000 ) ) ;
#16018=CARTESIAN_POINT ( 'NONE',  ( -7.500000000000000000, -4.330127018922199866, -1.000000000000000888 ) ) ;
#16019=CARTESIAN_POINT ( 'NONE',  ( 7.499999999999999112, -4.330127018922205195, -1.000000000000000888 ) ) ;
#16098=SHAPE_REPRESENTATION ( 'hex flange nut gradea_iso_ISO - 4161 - M10 - N', ( #2404 ), #11614 ) ;
#16124=CARTESIAN_POINT ( 'NONE',  ( 7.808623696107882317, -4.508310992946666040, -7.999704684617485739 ) ) ;
#16130=CARTESIAN_POINT ( 'NONE',  ( 7.894958282449824338, -1.603399432398892266, -7.593838100136980351 ) ) ;
#16155=VERTEX_POINT ( 'NONE', #24745 ) ;
#16157=CARTESIAN_POINT ( 'NONE',  ( 0.000000000000000000, 0.000000000000000000, -0.5776712190230133270 ) ) ;
#16177=CARTESIAN_POINT ( 'NONE',  ( 3.750000000000005329, 6.495190528383288253, 0.000000000000000000 ) ) ;
#16204=FACE_OUTER_BOUND ( 'NONE', #17679, .T. ) ;
#16222=EDGE_LOOP ( 'NONE', ( #11220, #18050, #28827, #14646, #10967 ) ) ;
#16228=CARTESIAN_POINT ( 'NONE',  ( 0.6249999999999994449, -8.299410119600885594, -7.298562697733110838 ) ) ;
#16248=CARTESIAN_POINT ( 'NONE',  ( 0.3306966981845720355, 8.469326210127405830, -7.349897473153450989 ) ) ;
#16273=DIRECTION ( 'NONE',  ( -0.5000000000000005551, 0.8660254037844383745, 0.000000000000000000 ) ) ;
#16294=FACE_OUTER_BOUND ( 'NONE', #3317, .T. ) ;
#16301=CARTESIAN_POINT ( 'NONE',  ( 7.908230272950877549, -3.123266379887881250, -7.776722524729575703 ) ) ;
#16321=EDGE_CURVE ( 'NONE', #12674, #24452, #17071, .T. ) ;
#16338=CARTESIAN_POINT ( 'NONE',  ( 7.779103221381273414, -4.168986698926031131, -7.929128246061905472 ) ) ;
#16342=CARTESIAN_POINT ( 'NONE',  ( -7.500000000000000000, -1.486698507076798847, -0.09861472150523968583 ) ) ;
#16459=CARTESIAN_POINT ( 'NONE',  ( 0.6250000000000013323, 8.299410119600871383, -7.298562697733108173 ) ) ;
#16476=CARTESIAN_POINT ( 'NONE',  ( 6.602753909532903087, 5.319290460493537154, -7.792447862505332168 ) ) ;
#16507=CARTESIAN_POINT ( 'NONE',  ( 4.406466114817131796, -6.116179640279303165, -7.446478553994418270 ) ) ;
#16511=CARTESIAN_POINT ( 'NONE',  ( -7.500000000000000888, -3.640541674360520119, -0.7158139487964623182 ) ) ;
#16516=ORIENTED_EDGE ( 'NONE', *, *, #33319, .F. ) ;
#16537=CARTESIAN_POINT ( 'NONE',  ( 7.703928834700305650, 4.447865386531936416, -7.917997657324733929 ) ) ;
#16561=CARTESIAN_POINT ( 'NONE',  ( 0.3483149870578491347, -8.861353789385031376, -7.493854785173814648 ) ) ;
#16628=CARTESIAN_POINT ( 'NONE',  ( 0.000000000000000000, 0.000000000000000000, -10.00000000000000000 ) ) ;
#16632=CARTESIAN_POINT ( 'NONE',  ( 7.499999999999999112, 0.7577384720672989404, -7.446470314338469620 ) ) ;
#16706=CARTESIAN_POINT ( 'NONE',  ( 7.500000000000000000, 4.330127018922190096, -7.422398894150032511 ) ) ;
#16723=CARTESIAN_POINT ( 'NONE',  ( -4.613983237546153582, 6.452243898629808960, -7.591546097228401457 ) ) ;
#16727=CARTESIAN_POINT ( 'NONE',  ( -2.352990130084580066E-16, 8.660254037844390851, -10.00000000000000000 ) ) ;
#16779=CARTESIAN_POINT ( 'NONE',  ( 0.000000000000000000, 0.000000000000000000, -8.499999999999998224 ) ) ;
#16827=CARTESIAN_POINT ( 'NONE',  ( 7.922281120364393914, -4.573931137438282057, -8.047472243342932430 ) ) ;
#16834=CARTESIAN_POINT ( 'NONE',  ( -5.007715329123872641E-16, -8.660254037844399733, -7.422398894150038728 ) ) ;
#16875=CARTESIAN_POINT ( 'NONE',  ( -7.500000000000000000, -4.330127018922198090, -7.422398894150034288 ) ) ;
#16879=CARTESIAN_POINT ( 'NONE',  ( 7.500000000000000888, -2.886751345948134873, -7.198902722707428481 ) ) ;
#16922=B_SPLINE_CURVE_WITH_KNOTS ( 'NONE', 3,
 ( #26355, #12745, #21073, #2523, #18689, #7640 ),
 .UNSPECIFIED., .F., .F.,
 ( 4, 2, 4 ),
 ( 0.004615310220740742597, 0.006918661718823353700, 0.009222013216905964803 ),
 .UNSPECIFIED. ) ;
#16934=VERTEX_POINT ( 'NONE', #27085 ) ;
#16944=ORIENTED_EDGE ( 'NONE', *, *, #33019, .T. ) ;
#16967=CARTESIAN_POINT ( 'NONE',  ( 4.174999999999999822, 0.000000000000000000, -0.5776712190230133270 ) ) ;
#16980=ORIENTED_EDGE ( 'NONE', *, *, #33450, .F. ) ;
#17045=DIRECTION ( 'NONE',  ( 1.000000000000000000, 0.000000000000000000, 0.000000000000000000 ) ) ;
#17063=CARTESIAN_POINT ( 'NONE',  ( -7.264118654998712010, 4.945491722146218905, -7.907633014911216840 ) ) ;
#17071=LINE ( 'NONE', #16727, #6169 ) ;
#17074=ORIENTED_EDGE ( 'NONE', *, *, #23752, .F. ) ;
#17084=EDGE_CURVE ( 'NONE', #854, #14265, #21218, .T. ) ;
#17093=AXIS2_PLACEMENT_3D ( 'NONE', #6835, #4275, #30178 ) ;
#17114=ORIENTED_EDGE ( 'NONE', *, *, #29470, .T. ) ;
#17129=EDGE_LOOP ( 'NONE', ( #22024, #17460, #4760, #10397 ) ) ;
#17173=ADVANCED_FACE ( 'NONE', ( #11170 ), #21381, .T. ) ;
#17243=AXIS2_PLACEMENT_3D ( 'NONE', #25709, #28441, #10225 ) ;
#17248=CARTESIAN_POINT ( 'NONE',  ( -1.994931997373328159E-14, -8.660254037844390851, -1.000000000000000888 ) ) ;
#17309=CARTESIAN_POINT ( 'NONE',  ( -7.549004593702459687, 4.358419834287835748, -7.700121441565839220 ) ) ;
#17401=CARTESIAN_POINT ( 'NONE',  ( -0.6511518506208974211, 8.763486134561267349, -7.907570769506047981 ) ) ;
#17405=( BOUNDED_SURFACE ( )  B_SPLINE_SURFACE ( 3, 2, ( 
 ( #15221, #30046, #32761 ),
 ( #19825, #7393, #17774 ),
 ( #27489, #25611, #6712 ),
 ( #2277, #4144, #14538 ),
 ( #33110, #22721, #9776 ),
 ( #14878, #17607, #30557 ),
 ( #15047, #2115, #1759 ),
 ( #27997, #9433, #1597 ) ),
 .UNSPECIFIED., .F., .F., .T. ) 
 B_SPLINE_SURFACE_WITH_KNOTS ( ( 4, 2, 2, 4 ),
 ( 3, 3 ),
 ( 0.03861844051980969916, 0.04325213341840641879, 0.04556897986770477860, 0.04788582631700313841 ),
 ( 0.000000000000000000, 1.000000000000000000 ),
 .UNSPECIFIED. ) 
 GEOMETRIC_REPRESENTATION_ITEM ( )  RATIONAL_B_SPLINE_SURFACE ( (
 ( 1.000000000000000000, 0.8047781759831920123, 1.000000000000000000),
 ( 1.000000000000000000, 0.8123762462803147955, 1.000000000000000000),
 ( 1.000000000000000000, 0.8190659850619289584, 1.000000000000000000),
 ( 1.000000000000000000, 0.8191937571012362085, 1.000000000000000000),
 ( 1.000000000000000000, 0.8176092952779873135, 1.000000000000000000),
 ( 1.000000000000000000, 0.8122962088597077690, 1.000000000000000000),
 ( 1.000000000000000000, 0.8086311330827508081, 1.000000000000000000),
 ( 1.000000000000000000, 0.8047712282214326551, 1.000000000000000000) ) ) 
 REPRESENTATION_ITEM ( '' )  SURFACE ( )  );
#17460=ORIENTED_EDGE ( 'NONE', *, *, #30591, .T. ) ;
#17472=CARTESIAN_POINT ( 'NONE',  ( -7.500000000000000000, 4.330127018922191873, -10.00000000000000000 ) ) ;
#17539=VERTEX_POINT ( 'NONE', #24787 ) ;
#17552=CARTESIAN_POINT ( 'NONE',  ( 0.000000000000000000, 0.000000000000000000, 0.000000000000000000 ) ) ;
#17561=CARTESIAN_POINT ( 'NONE',  ( 4.250000000000000000, 0.000000000000000000, -0.5251556536572846712 ) ) ;
#17607=CARTESIAN_POINT ( 'NONE',  ( -6.439685834476978954, 4.942299687812971243, -7.659344964963200830 ) ) ;
#17615=ORIENTED_EDGE ( 'NONE', *, *, #32268, .F. ) ;
#17625=CARTESIAN_POINT ( 'NONE',  ( 4.336808689942017736E-16, 8.660254037844390851, -1.000000000000000888 ) ) ;
#17633=ORIENTED_EDGE ( 'NONE', *, *, #5778, .T. ) ;
#17639=DIRECTION ( 'NONE',  ( -0.000000000000000000, -0.000000000000000000, 1.000000000000000000 ) ) ;
#17679=EDGE_LOOP ( 'NONE', ( #29731, #21503, #26377, #14733 ) ) ;
#17722=ORIENTED_EDGE ( 'NONE', *, *, #4731, .T. ) ;
#17759=ORIENTED_EDGE ( 'NONE', *, *, #12049, .T. ) ;
#17774=CARTESIAN_POINT ( 'NONE',  ( -1.249327701954873415, 8.410337540189265937, -7.776713651267812999 ) ) ;
#17802=FACE_OUTER_BOUND ( 'NONE', #19208, .T. ) ;
#17813=CARTESIAN_POINT ( 'NONE',  ( -1.250000000000000444, 7.938566201357357244, -7.198902722707429369 ) ) ;
#17838=AXIS2_PLACEMENT_3D ( 'NONE', #7861, #5461, #13128 ) ;
#17844=CARTESIAN_POINT ( 'NONE',  ( -7.499999999999999112, 4.651022038490018495, -7.928862870699868282 ) ) ;
#17852=DIRECTION ( 'NONE',  ( 1.000000000000000000, 0.000000000000000000, 0.000000000000000000 ) ) ;
#17858=CONICAL_SURFACE ( 'NONE', #21137, 5.000000000000001776, 0.9599310885968795892 ) ;
#17899=CARTESIAN_POINT ( 'NONE',  ( -3.280815508853482498, -7.221948645665452915, -7.591546097228404122 ) ) ;
#17914=CARTESIAN_POINT ( 'NONE',  ( -0.2779000157839473517, -8.820699686765063774, -7.928862157988305626 ) ) ;
#17958=EDGE_CURVE ( 'NONE', #12741, #23132, #10165, .T. ) ;
#17961=ORIENTED_EDGE ( 'NONE', *, *, #14161, .T. ) ;
#18019=CARTESIAN_POINT ( 'NONE',  ( -7.922798540899431252, 4.627424769998836673, -8.057412477672047046 ) ) ;
#18050=ORIENTED_EDGE ( 'NONE', *, *, #8553, .F. ) ;
#18153=CARTESIAN_POINT ( 'NONE',  ( -7.500000000000000000, -4.330127018922198090, -10.00000000000000000 ) ) ;
#18155=DIRECTION ( 'NONE',  ( 1.000000000000000000, 0.000000000000000000, 0.000000000000000000 ) ) ;
#18189=CARTESIAN_POINT ( 'NONE',  ( -7.500000000000000000, -4.732323933430407692, -7.493854309896101462 ) ) ;
#18218=B_SPLINE_CURVE_WITH_KNOTS ( 'NONE', 3,
 ( #26721, #31834, #3383, #511, #667, #21281, #13778, #11070, #21610, #8500 ),
 .UNSPECIFIED., .F., .F.,
 ( 4, 2, 2, 2, 4 ),
 ( 0.000000000000000000, 0.002305503304226490767, 0.004611006608452981534, 0.006916509912679473168, 0.009222013216905964803 ),
 .UNSPECIFIED. ) ;
#18243=CARTESIAN_POINT ( 'NONE',  ( -4.406842699996122548, 6.115962218725288224, 1.165517335421917267E-15 ) ) ;
#18305=ORIENTED_EDGE ( 'NONE', *, *, #6476, .F. ) ;
#18307=CARTESIAN_POINT ( 'NONE',  ( 7.500000000000001776, 0.000000000000000000, 0.000000000000000000 ) ) ;
#18347=CIRCLE ( 'NONE', #920, 0.7733184030943203169 ) ;
#18350=CARTESIAN_POINT ( 'NONE',  ( -6.902527771671634227, -4.675077770780906583, -0.7026937717022867513 ) ) ;
#18359=CARTESIAN_POINT ( 'NONE',  ( -4.250000000000000000, 5.204748896376250699E-16, -0.5251556536572846712 ) ) ;
#18424=ADVANCED_FACE ( 'NONE', ( #29397 ), #30076, .T. ) ;
#18449=CARTESIAN_POINT ( 'NONE',  ( -3.750000000000007105, -6.495190528383289141, 0.000000000000000000 ) ) ;
#18459=VERTEX_POINT ( 'NONE', #24792 ) ;
#18481=CARTESIAN_POINT ( 'NONE',  ( 5.335963852943280017, 6.035591050531201596, -7.593821156097048330 ) ) ;
#18529=CARTESIAN_POINT ( 'NONE',  ( 0.000000000000000000, 0.000000000000000000, 0.000000000000000000 ) ) ;
#18538=CARTESIAN_POINT ( 'NONE',  ( 7.500000000000000000, 0.7723602884954153813, -7.026388801733942202 ) ) ;
#18555=CARTESIAN_POINT ( 'NONE',  ( -5.007715329123872641E-16, -8.660254037844399733, -7.422398894150038728 ) ) ;
#18601=B_SPLINE_CURVE_WITH_KNOTS ( 'NONE', 3,
 ( #16177, #19907, #14796, #22467, #27747, #6631 ),
 .UNSPECIFIED., .F., .F.,
 ( 4, 2, 4 ),
 ( 0.004444412883774346255, 0.006655097293744437204, 0.008865781703714529019 ),
 .UNSPECIFIED. ) ;
#18621=EDGE_LOOP ( 'NONE', ( #21889, #17961, #31617 ) ) ;
#18641=CARTESIAN_POINT ( 'NONE',  ( 2.621328321948289020, 7.606199919103058704, -7.633618187056857352 ) ) ;
#18689=CARTESIAN_POINT ( 'NONE',  ( 7.914984360234579519, -3.818534719232097974, -7.907701344400643428 ) ) ;
#18690=MECHANICAL_DESIGN_GEOMETRIC_PRESENTATION_REPRESENTATION('',(#14337),#3944);
#18703=CARTESIAN_POINT ( 'NONE',  ( 7.894787914004607998, 0.7661396099416312166, -7.591390474663430865 ) ) ;
#18744=EDGE_CURVE ( 'NONE', #24712, #8601, #6897, .T. ) ;
#18749=CARTESIAN_POINT ( 'NONE',  ( -7.500000000000000888, -3.608439182435167591, -7.298562697733108173 ) ) ;
#18762=ORIENTED_EDGE ( 'NONE', *, *, #24061, .F. ) ;
#18791=CARTESIAN_POINT ( 'NONE',  ( -0.6169862416623524970, -8.783631307150855605, -7.913704048099795330 ) ) ;
#18834=ORIENTED_EDGE ( 'NONE', *, *, #25804, .T. ) ;
#18841=B_SPLINE_CURVE_WITH_KNOTS ( 'NONE', 3,
 ( #16834, #29623, #32165, #6454, #31672, #8341 ),
 .UNSPECIFIED., .F., .F.,
 ( 4, 2, 4 ),
 ( 0.000000000000000000, 0.0004189869898914152461, 0.0008379739797828304922 ),
 .UNSPECIFIED. ) ;
#18854=CARTESIAN_POINT ( 'NONE',  ( 0.5984201754795568373, 8.314755988442765755, -0.7022220667781353676 ) ) ;
#18858=CARTESIAN_POINT ( 'NONE',  ( 7.922798488042200660, -4.627419312545550056, -8.057411459260041653 ) ) ;
#18869=FACE_BOUND ( 'NONE', #19387, .T. ) ;
#18872=AXIS2_PLACEMENT_3D ( 'NONE', #22491, #4608, #32535 ) ;
#18880=EDGE_CURVE ( 'NONE', #33504, #14265, #6167, .T. ) ;
#18901=CARTESIAN_POINT ( 'NONE',  ( 4.599534470797546959, -6.460478697736932396, -7.590212325761396706 ) ) ;
#18907=CARTESIAN_POINT ( 'NONE',  ( -7.500000000000000000, -3.988190556646204588, -0.8526458641284329065 ) ) ;
#18918=AXIS2_PLACEMENT_3D ( 'NONE', #19888, #11725, #32333 ) ;
#18959=CARTESIAN_POINT ( 'NONE',  ( 6.250000000000000000, -5.051814855409237026, -7.198902722707430257 ) ) ;
#18976=CARTESIAN_POINT ( 'NONE',  ( 1.013163106016871096, 8.075304045852551127, -7.231838333420561149 ) ) ;
#18977=CIRCLE ( 'NONE', #10819, 0.7733184030943203169 ) ;
#19041=ORIENTED_EDGE ( 'NONE', *, *, #4823, .F. ) ;
#19075=CARTESIAN_POINT ( 'NONE',  ( -7.500000000000000000, 3.608439182435158710, -7.298562697733104621 ) ) ;
#19091=ORIENTED_EDGE ( 'NONE', *, *, #24061, .T. ) ;
#19101=AXIS2_PLACEMENT_3D ( 'NONE', #18529, #3018, #26359 ) ;
#19102=CARTESIAN_POINT ( 'NONE',  ( 0.000000000000000000, 0.000000000000000000, 0.000000000000000000 ) ) ;
#19178=AXIS2_PLACEMENT_3D ( 'NONE', #17472, #4529, #1974 ) ;
#19196=CARTESIAN_POINT ( 'NONE',  ( 7.922811941611899833, 4.628808333142401032, -8.057670691780701944 ) ) ;
#19208=EDGE_LOOP ( 'NONE', ( #3296, #17074, #19091, #18305 ) ) ;
#19216=VECTOR ( 'NONE', #31100, 1000.000000000000000 ) ;
#19237=SURFACE_SIDE_STYLE ('',( #8835 ) ) ;
#19291=CARTESIAN_POINT ( 'NONE',  ( -1.060314165522979968, -8.048081368954337123, -7.659344964963557878 ) ) ;
#19301=VERTEX_POINT ( 'NONE', #11968 ) ;
#19384=EDGE_CURVE ( 'NONE', #22574, #29479, #19765, .T. ) ;
#19387=EDGE_LOOP ( 'NONE', ( #7026, #20769 ) ) ;
#19406=LINE ( 'NONE', #22634, #32831 ) ;
#19450=CARTESIAN_POINT ( 'NONE',  ( -7.922281120364393914, 4.573931137438271399, -8.047472243342930653 ) ) ;
#19614=AXIS2_PLACEMENT_3D ( 'NONE', #16157, #27897, #22618 ) ;
#19636=UNCERTAINTY_MEASURE_WITH_UNIT (LENGTH_MEASURE( 1.000000000000000082E-05 ), #22758, 'distance_accuracy_value', 'NONE');
#19675=EDGE_LOOP ( 'NONE', ( #28022, #33257, #8050, #30633 ) ) ;
#19714=ORIENTED_EDGE ( 'NONE', *, *, #6868, .F. ) ;
#19765=CIRCLE ( 'NONE', #27394, 5.000000000000000888 ) ;
#19825=CARTESIAN_POINT ( 'NONE',  ( -0.9763930676156993282, 8.096533237421580154, -7.213065638943424673 ) ) ;
#19858=CARTESIAN_POINT ( 'NONE',  ( -7.922281120364393914, 4.573931137438271399, -8.047472243342930653 ) ) ;
#19875=CARTESIAN_POINT ( 'NONE',  ( 0.6508621380849231031, 8.763657152406445050, -7.907633014911220393 ) ) ;
#19888=CARTESIAN_POINT ( 'NONE',  ( -14.99999999999998934, -1.734723475976807094E-15, -10.00000000000000000 ) ) ;
#19891=DIRECTION ( 'NONE',  ( 0.9396926207859143121, 1.150791560227857665E-16, -0.3420201433256525592 ) ) ;
#19907=CARTESIAN_POINT ( 'NONE',  ( 4.403473400622098133, 6.117907484625861869, 2.043043468777371629E-15 ) ) ;
#19912=VERTEX_POINT ( 'NONE', #22142 ) ;
#19972=CARTESIAN_POINT ( 'NONE',  ( -2.452879891156814818, -7.244083172395189507, -0.1007566405101857632 ) ) ;
#20017=ORIENTED_EDGE ( 'NONE', *, *, #3133, .F. ) ;
#20050=ORIENTED_EDGE ( 'NONE', *, *, #29682, .T. ) ;
#20074=VECTOR ( 'NONE', #13135, 1000.000000000000000 ) ;
#20126=CARTESIAN_POINT ( 'NONE',  ( -7.500000000000000000, -4.330127018922198090, -7.422398894150034288 ) ) ;
#20178=CARTESIAN_POINT ( 'NONE',  ( -2.459698528280933161, 7.240146430416066536, -0.09933465333851029810 ) ) ;
#20187=CARTESIAN_POINT ( 'NONE',  ( 6.484173630542770184, 4.916614646782027087, -7.642786413619098163 ) ) ;
#20190=DIRECTION ( 'NONE',  ( 1.000000000000000000, 0.000000000000000000, 0.000000000000000000 ) ) ;
#20225=DIRECTION ( 'NONE',  ( 0.000000000000000000, 0.000000000000000000, -1.000000000000000000 ) ) ;
#20300=EDGE_CURVE ( 'NONE', #23132, #18459, #8916, .T. ) ;
#20318=CARTESIAN_POINT ( 'NONE',  ( 7.499999999999999112, 1.854554393013827296, -0.1880126015361732184 ) ) ;
#20345=EDGE_CURVE ( 'NONE', #6342, #4633, #15446, .T. ) ;
#20412=CARTESIAN_POINT ( 'NONE',  ( 7.500000000000001776, 0.000000000000000000, 0.000000000000000000 ) ) ;
#20440=EDGE_CURVE ( 'NONE', #16934, #33504, #14102, .T. ) ;
#20541=CARTESIAN_POINT ( 'NONE',  ( -5.000000000000000888, 5.773502691896258199, -7.063244554130002406 ) ) ;
#20601=EDGE_LOOP ( 'NONE', ( #15608, #4467, #24459 ) ) ;
#20623=FACE_OUTER_BOUND ( 'NONE', #28991, .T. ) ;
#20629=SHAPE_DEFINITION_REPRESENTATION ( #15154, #16098 ) ;
#20632=LINE ( 'NONE', #15346, #3914 ) ;
#20738=CARTESIAN_POINT ( 'NONE',  ( -7.500000000000346390, -3.105855721450154316, -7.659356991636309786 ) ) ;
#20769=ORIENTED_EDGE ( 'NONE', *, *, #4731, .F. ) ;
#20772=CARTESIAN_POINT ( 'NONE',  ( -7.894787914004607998, -1.230850257101226302E-13, -7.591390474663425536 ) ) ;
#20863=EDGE_CURVE ( 'NONE', #6342, #27806, #1980, .T. ) ;
#20867=CARTESIAN_POINT ( 'NONE',  ( -0.2791032213812780771, 8.821394357840562250, -7.929128246061909024 ) ) ;
#20871=LINE ( 'NONE', #18153, #19216 ) ;
#20873=CARTESIAN_POINT ( 'NONE',  ( 1.211595439868046853, -7.960739084487661543, -0.4504974108212073114 ) ) ;
#20902=CARTESIAN_POINT ( 'NONE',  ( -2.352990130084580066E-16, 8.660254037844390851, -7.422398894150034288 ) ) ;
#20952=CARTESIAN_POINT ( 'NONE',  ( -10.12668159690567649, 1.256356190803088863E-15, -9.999999999999998224 ) ) ;
#20980=ORIENTED_EDGE ( 'NONE', *, *, #6811, .T. ) ;
#21064=ORIENTED_EDGE ( 'NONE', *, *, #17084, .T. ) ;
#21071=CONICAL_SURFACE ( 'NONE', #407, 7.500000000000001776, 0.8594454914424796144 ) ;
#21073=CARTESIAN_POINT ( 'NONE',  ( 7.897850199329715437, -1.533397866934079312, -7.634054012537967893 ) ) ;
#21084=CARTESIAN_POINT ( 'NONE',  ( 7.500000000000000000, 1.572594658376109011, -7.069792055233639516 ) ) ;
#21095=AXIS2_PLACEMENT_3D ( 'NONE', #22201, #11980, #14198 ) ;
#21130=CARTESIAN_POINT ( 'NONE',  ( -7.500000000000001776, 0.000000000000000000, 0.000000000000000000 ) ) ;
#21137=AXIS2_PLACEMENT_3D ( 'NONE', #5065, #20225, #13069 ) ;
#21167=APPLICATION_CONTEXT ( 'automotive_design' ) ;
#21175=CARTESIAN_POINT ( 'NONE',  ( 0.2791032213812723040, -8.821394357840571132, -7.929128246061910801 ) ) ;
#21191=CARTESIAN_POINT ( 'NONE',  ( 0.6169862416622686752, 8.783631307150953305, -7.913704048099833521 ) ) ;
#21195=DIRECTION ( 'NONE',  ( 1.000000000000000000, 0.000000000000000000, 0.000000000000000000 ) ) ;
#21214=EDGE_LOOP ( 'NONE', ( #20980, #26707, #18762, #5024 ) ) ;
#21218=LINE ( 'NONE', #442, #22436 ) ;
#21241=CARTESIAN_POINT ( 'NONE',  ( 10.12668159690567649, 0.000000000000000000, -9.999999999999998224 ) ) ;
#21246=CARTESIAN_POINT ( 'NONE',  ( 3.093157300003884558, 6.874418838041288282, 2.127746763502802452E-15 ) ) ;
#21250=CARTESIAN_POINT ( 'NONE',  ( 7.499999999998625100, 3.882635837268474166, -7.781684861371460649 ) ) ;
#21281=CARTESIAN_POINT ( 'NONE',  ( 3.288228914120474133, -7.217643567644815406, -7.591235721156641247 ) ) ;
#21336=CARTESIAN_POINT ( 'NONE',  ( -6.658902113226115027, -5.287118297636088649, -7.776713651266535798 ) ) ;
#21339=AXIS2_PLACEMENT_3D ( 'NONE', #29751, #31961, #21741 ) ;
#21349=EDGE_CURVE ( 'NONE', #19912, #6342, #13729, .T. ) ;
#21381=PLANE ( 'NONE',  #25159 ) ;
#21384=ORIENTED_EDGE ( 'NONE', *, *, #31618, .T. ) ;
#21396=ORIENTED_EDGE ( 'NONE', *, *, #7071, .F. ) ;
#21406=COLOUR_RGB ( '', 0.72549020, 0.75294118, 0.79215686) ;
#21417=CARTESIAN_POINT ( 'NONE',  ( -5.000000000000000888, 6.123233995736767268E-16, 0.000000000000000000 ) ) ;
#21432=EDGE_LOOP ( 'NONE', ( #28521, #11173, #8998, #22016, #30832, #7999 ) ) ;
#21434=VERTEX_POINT ( 'NONE', #7202 ) ;
#21461=CARTESIAN_POINT ( 'NONE',  ( 2.352174619736673744, -7.302225387959338399, -7.450218641350605076 ) ) ;
#21466=CARTESIAN_POINT ( 'NONE',  ( -7.500000000000000000, -2.886751345948133984, -7.198902722707428481 ) ) ;
#21503=ORIENTED_EDGE ( 'NONE', *, *, #7071, .T. ) ;
#21523=CARTESIAN_POINT ( 'NONE',  ( 1.060314165522845187, 8.048081368953960535, -7.659344964963204383 ) ) ;
#21571=CARTESIAN_POINT ( 'NONE',  ( 2.500000000000000444, 7.216878364870322748, -7.063244554130000630 ) ) ;
#21610=CARTESIAN_POINT ( 'NONE',  ( 0.6511518506208960888, -8.763486134561278007, -7.907570769506051533 ) ) ;
#21620=CARTESIAN_POINT ( 'NONE',  ( 5.276498195232308674, -6.073236878017951312, -7.633618187056764981 ) ) ;
#21626=CARTESIAN_POINT ( 'NONE',  ( 3.750000000000005329, 6.495190528383288253, 0.000000000000000000 ) ) ;
#21653=DIRECTION ( 'NONE',  ( -1.000000000000000000, 1.224646799147354686E-16, 0.000000000000000000 ) ) ;
#21680=FACE_OUTER_BOUND ( 'NONE', #13029, .T. ) ;
#21706=ORIENTED_EDGE ( 'NONE', *, *, #1569, .T. ) ;
#21731=AXIS2_PLACEMENT_3D ( 'NONE', #31891, #392, #3112 ) ;
#21741=DIRECTION ( 'NONE',  ( -1.000000000000000000, 0.000000000000000000, 0.000000000000000000 ) ) ;
#21747=CARTESIAN_POINT ( 'NONE',  ( 7.499999999999999112, 4.652409454067514716, -7.929128589908465585 ) ) ;
#21773=CARTESIAN_POINT ( 'NONE',  ( 7.500000000000000000, 4.330127018922190096, -10.00000000000000000 ) ) ;
#21838=CARTESIAN_POINT ( 'NONE',  ( -5.007715329123872641E-16, -8.660254037844399733, -7.422398894150038728 ) ) ;
#21889=ORIENTED_EDGE ( 'NONE', *, *, #1797, .F. ) ;
#21894=ORIENTED_EDGE ( 'NONE', *, *, #14599, .T. ) ;
#21908=DIRECTION ( 'NONE',  ( 1.000000000000000000, 0.000000000000000000, 0.000000000000000000 ) ) ;
#21925=CARTESIAN_POINT ( 'NONE',  ( 5.274401269815139237, 6.074457022762083547, -7.633824513837111247 ) ) ;
#21956=B_SPLINE_CURVE_WITH_KNOTS ( 'NONE', 3,
 ( #30599, #7264, #17813, #2663, #4870, #20541, #30943, #31443, #100 ),
 .UNSPECIFIED., .F., .F.,
 ( 4, 2, 1, 2, 4 ),
 ( 0.000000000000000000, 0.002165063509461098365, 0.004330127018922195863, 0.006495190528383293360, 0.008660254037844389990 ),
 .UNSPECIFIED. ) ;
#21960=CARTESIAN_POINT ( 'NONE',  ( 1.015826369459276846, -8.073766409988136772, -7.642786413614194529 ) ) ;
#21997=CARTESIAN_POINT ( 'NONE',  ( 7.499999999999999112, -1.443375672974070323, -7.063244554130001518 ) ) ;
#22002=CARTESIAN_POINT ( 'NONE',  ( -7.500000000000000000, -4.330127018922198090, -7.422398894150034288 ) ) ;
#22016=ORIENTED_EDGE ( 'NONE', *, *, #4607, .T. ) ;
#22024=ORIENTED_EDGE ( 'NONE', *, *, #2094, .F. ) ;
#22095=CARTESIAN_POINT ( 'NONE',  ( 7.263825692932297962, 4.945657111639574666, -7.907570769506046204 ) ) ;
#22140=ORIENTED_EDGE ( 'NONE', *, *, #30412, .T. ) ;
#22142=CARTESIAN_POINT ( 'NONE',  ( -1.994931997373328159E-14, -8.660254037844390851, -1.000000000000000888 ) ) ;
#22194=ORIENTED_EDGE ( 'NONE', *, *, #22411, .T. ) ;
#22201=CARTESIAN_POINT ( 'NONE',  ( 0.000000000000000000, 0.000000000000000000, -10.00000000000000000 ) ) ;
#22203=PRODUCT ( 'hex flange nut gradea_iso_ISO - 4161 - M10 - N', 'hex flange nut gradea_iso_ISO - 4161 - M10 - N', '', ( #28120 ) ) ;
#22282=EDGE_LOOP ( 'NONE', ( #11101, #1489, #17722, #22393 ) ) ;
#22306=ORIENTED_EDGE ( 'NONE', *, *, #30591, .F. ) ;
#22372=FACE_OUTER_BOUND ( 'NONE', #21214, .T. ) ;
#22393=ORIENTED_EDGE ( 'NONE', *, *, #29682, .F. ) ;
#22402=CARTESIAN_POINT ( 'NONE',  ( -7.499999999999999112, 0.3744244963005040061, 1.590163186312071526E-15 ) ) ;
#22405=ADVANCED_FACE ( 'NONE', ( #21680 ), #12391, .F. ) ;
#22411=EDGE_CURVE ( 'NONE', #25547, #24712, #14681, .T. ) ;
#22418=DIRECTION ( 'NONE',  ( 0.8191520442889907994, 0.000000000000000000, 0.5735764363510474917 ) ) ;
#22436=VECTOR ( 'NONE', #26005, 1000.000000000000000 ) ;
#22439=CARTESIAN_POINT ( 'NONE',  ( -10.39117206796836079, 0.000000000000000000, -8.499999999999998224 ) ) ;
#22467=CARTESIAN_POINT ( 'NONE',  ( 6.288404560131952259, 5.029641972278931839, -0.4504974108211943773 ) ) ;
#22491=CARTESIAN_POINT ( 'NONE',  ( -5.007715329123872641E-16, -8.660254037844399733, -10.00000000000000000 ) ) ;
#22531=TOROIDAL_SURFACE ( 'NONE', #5122, 10.12668159690567649, 0.7733184030943209830 ) ;
#22574=VERTEX_POINT ( 'NONE', #14508 ) ;
#22618=DIRECTION ( 'NONE',  ( 1.000000000000000000, 0.000000000000000000, 0.000000000000000000 ) ) ;
#22634=CARTESIAN_POINT ( 'NONE',  ( 4.250000000000000000, 0.000000000000000000, -10.00000000000000000 ) ) ;
#22643=EDGE_CURVE ( 'NONE', #7575, #19301, #30192, .T. ) ;
#22690=EDGE_LOOP ( 'NONE', ( #29312, #8096, #8482, #28365 ) ) ;
#22712=DIRECTION ( 'NONE',  ( 0.000000000000000000, 0.000000000000000000, -1.000000000000000000 ) ) ;
#22721=CARTESIAN_POINT ( 'NONE',  ( -5.088535779737005882, 5.722386535631696525, -7.491772860716161553 ) ) ;
#22742=CARTESIAN_POINT ( 'NONE',  ( 7.500000000000000000, -4.330127018922199866, -10.00000000000000000 ) ) ;
#22750=CARTESIAN_POINT ( 'NONE',  ( 6.523606932381168733, 4.893847819346807348, -7.213065638943126245 ) ) ;
#22754=CARTESIAN_POINT ( 'NONE',  ( 0.000000000000000000, 0.000000000000000000, -8.499999999999998224 ) ) ;
#22758=( LENGTH_UNIT ( ) NAMED_UNIT ( * ) SI_UNIT ( .MILLI., .METRE. ) );
#22819=CIRCLE ( 'NONE', #21731, 7.500000000000001776 ) ;
#22854=DIRECTION ( 'NONE',  ( 0.5000000000000006661, 0.8660254037844383745, -0.000000000000000000 ) ) ;
#22855=CARTESIAN_POINT ( 'NONE',  ( -6.250000000000000000, -5.051814855409233473, -7.198902722707430257 ) ) ;
#22861=CARTESIAN_POINT ( 'NONE',  ( 7.894787914004607998, 1.243647571710251278E-13, -7.591390474663425536 ) ) ;
#22909=VERTEX_POINT ( 'NONE', #22861 ) ;
#22948=ORIENTED_EDGE ( 'NONE', *, *, #32658, .F. ) ;
#22954=CARTESIAN_POINT ( 'NONE',  ( -6.288404560131954923, -5.029641972278938944, -0.4504974108212008721 ) ) ;
#23043=CARTESIAN_POINT ( 'NONE',  ( 7.500000000000000888, 1.489914625144004523, -0.1187923833806749097 ) ) ;
#23129=CARTESIAN_POINT ( 'NONE',  ( -7.499999999999650058, -0.7583608255766450812, -7.446489218764574147 ) ) ;
#23132=VERTEX_POINT ( 'NONE', #12088 ) ;
#23166=CARTESIAN_POINT ( 'NONE',  ( -7.922281120364393914, 4.573931137438271399, -8.047472243342930653 ) ) ;
#23175=CARTESIAN_POINT ( 'NONE',  ( -5.274401269815139237, -6.074457022762090652, -7.633824513837113912 ) ) ;
#23239=B_SPLINE_CURVE_WITH_KNOTS ( 'NONE', 3,
 ( #31800, #11363, #963, #26856, #6065, #21571, #26519, #16459, #3684 ),
 .UNSPECIFIED., .F., .F.,
 ( 4, 2, 1, 2, 4 ),
 ( 0.000000000000000000, 0.002165063509461097498, 0.004330127018922194995, 0.006495190528383292493, 0.008660254037844389990 ),
 .UNSPECIFIED. ) ;
#23277=CARTESIAN_POINT ( 'NONE',  ( -3.295171437451516638, -7.213553046160524396, -7.590212325761481971 ) ) ;
#23348=CARTESIAN_POINT ( 'NONE',  ( 7.499999999999999112, -4.330127018922205195, -1.000000000000000888 ) ) ;
#23350=DIRECTION ( 'NONE',  ( 1.000000000000000000, 0.000000000000000000, 0.000000000000000000 ) ) ;
#23359=CARTESIAN_POINT ( 'NONE',  ( -6.293430271071534854, 5.026740376715094882, -0.4524126574264483169 ) ) ;
#23369=CARTESIAN_POINT ( 'NONE',  ( -7.500000000000000000, 4.330127018922191873, -10.00000000000000000 ) ) ;
#23421=ADVANCED_FACE ( 'NONE', ( #33548 ), #29766, .T. ) ;
#23425=CARTESIAN_POINT ( 'NONE',  ( 3.093533885183100018, 6.874201416487501604, -7.446478553995813598 ) ) ;
#23489=ADVANCED_FACE ( 'NONE', ( #18869, #31981 ), #15816, .T. ) ;
#23511=EDGE_CURVE ( 'NONE', #3624, #30882, #18347, .T. ) ;
#23593=AXIS2_PLACEMENT_3D ( 'NONE', #14159, #6149, #26599 ) ;
#23631=CARTESIAN_POINT ( 'NONE',  ( -7.500000000000667910, 3.157052757790226316, -7.642767288269818771 ) ) ;
#23661=ORIENTED_EDGE ( 'NONE', *, *, #1569, .F. ) ;
#23671=CARTESIAN_POINT ( 'NONE',  ( -7.263825692932299738, -4.945657111639584436, -7.907570769506049757 ) ) ;
#23690=CARTESIAN_POINT ( 'NONE',  ( -7.500000000000000000, -3.469446951953614189E-15, -6.991905250253751980 ) ) ;
#23710=EDGE_LOOP ( 'NONE', ( #15706, #13771, #23661 ) ) ;
#23748=CARTESIAN_POINT ( 'NONE',  ( 7.500000000000000000, -3.988190556646209028, -0.8526458641284331286 ) ) ;
#23752=EDGE_CURVE ( 'NONE', #25811, #613, #1221, .T. ) ;
#23834=CARTESIAN_POINT ( 'NONE',  ( -7.500000000000000000, -4.330127018922198090, -10.00000000000000000 ) ) ;
#23862=AXIS2_PLACEMENT_3D ( 'NONE', #28112, #33051, #15168 ) ;
#23893=CIRCLE ( 'NONE', #21095, 5.000000000000000888 ) ;
#23901=CARTESIAN_POINT ( 'NONE',  ( -0.3306966981848578069, -8.469326210127253063, -7.349897473154448413 ) ) ;
#23919=DIRECTION ( 'NONE',  ( -0.000000000000000000, -0.000000000000000000, 1.000000000000000000 ) ) ;
#23962=CONICAL_SURFACE ( 'NONE', #14720, 4.174999999999999822, 0.9599310885968795892 ) ;
#24011=CARTESIAN_POINT ( 'NONE',  ( -7.922281120364393914, -4.573931137438277617, -8.047472243342932430 ) ) ;
#24032=ORIENTED_EDGE ( 'NONE', *, *, #18744, .T. ) ;
#24061=EDGE_CURVE ( 'NONE', #25811, #12674, #25245, .T. ) ;
#24062=CARTESIAN_POINT ( 'NONE',  ( -6.484173630544109557, -4.916614646775610886, -7.642786413610934915 ) ) ;
#24114=CARTESIAN_POINT ( 'NONE',  ( -2.352990130084580066E-16, 8.660254037844390851, -7.564335161054497547 ) ) ;
#24139=CARTESIAN_POINT ( 'NONE',  ( 7.894787914004607998, 1.243647571710251278E-13, -7.591390474663425536 ) ) ;
#24216=CARTESIAN_POINT ( 'NONE',  ( 7.500000000000000000, -4.330127018922199866, -7.422398894150035176 ) ) ;
#24299=CARTESIAN_POINT ( 'NONE',  ( 7.500000000000000000, 4.732328341851997244, -7.493855119309152713 ) ) ;
#24383=DIRECTION ( 'NONE',  ( 1.000000000000000000, 0.000000000000000000, 0.000000000000000000 ) ) ;
#24391=CARTESIAN_POINT ( 'NONE',  ( -7.500000000000000888, -4.330127018922198090, -7.564335161054497547 ) ) ;
#24407=CARTESIAN_POINT ( 'NONE',  ( -7.968863443239230016, -4.547634245050486079, -8.057411785091789014 ) ) ;
#24452=VERTEX_POINT ( 'NONE', #28194 ) ;
#24453=DIRECTION ( 'NONE',  ( -1.000000000000000000, 0.000000000000000000, 0.000000000000000000 ) ) ;
#24459=ORIENTED_EDGE ( 'NONE', *, *, #212, .F. ) ;
#24487=ORIENTED_EDGE ( 'NONE', *, *, #11621, .F. ) ;
#24537=ORIENTED_EDGE ( 'NONE', *, *, #30367, .T. ) ;
#24540=ORIENTED_EDGE ( 'NONE', *, *, #22643, .T. ) ;
#24549=CARTESIAN_POINT ( 'NONE',  ( 7.808623696107343193, 4.508310992947586193, -7.999704684617482187 ) ) ;
#24567=CARTESIAN_POINT ( 'NONE',  ( -3.288228914120473245, 7.217643567644804747, -7.591235721156635030 ) ) ;
#24570=( BOUNDED_SURFACE ( )  B_SPLINE_SURFACE ( 3, 2, ( 
 ( #33413, #17914, #28305 ),
 ( #11410, #21960, #6110 ),
 ( #3564, #21461, #5776 ),
 ( #5948, #16507, #18901 ),
 ( #27072, #5621, #21620 ),
 ( #3734, #10913, #26561 ),
 ( #29459, #32014, #13453 ),
 ( #31843, #16338, #3231 ) ),
 .UNSPECIFIED., .F., .F., .F. ) 
 B_SPLINE_SURFACE_WITH_KNOTS ( ( 4, 2, 2, 4 ),
 ( 3, 3 ),
 ( 0.03861844051980971304, 0.04325213341840643266, 0.04556897986770479247, 0.04788582631700314535 ),
 ( 0.000000000000000000, 1.000000000000000000 ),
 .UNSPECIFIED. ) 
 GEOMETRIC_REPRESENTATION_ITEM ( )  RATIONAL_B_SPLINE_SURFACE ( (
 ( 1.000000000000000000, 0.8047781759831919013, 1.000000000000000000),
 ( 1.000000000000000000, 0.8123762462802479600, 1.000000000000000000),
 ( 1.000000000000000000, 0.8190659850620179983, 1.000000000000000000),
 ( 1.000000000000000000, 0.8191937571011910224, 1.000000000000000000),
 ( 1.000000000000000000, 0.8176092952781196521, 1.000000000000000000),
 ( 1.000000000000000000, 0.8122962088595743202, 1.000000000000000000),
 ( 1.000000000000000000, 0.8086311330828506172, 1.000000000000000000),
 ( 1.000000000000000000, 0.8047712282214323221, 1.000000000000000000) ) ) 
 REPRESENTATION_ITEM ( '' )  SURFACE ( )  );
#24588=FACE_OUTER_BOUND ( 'NONE', #23710, .T. ) ;
#24674=PLANE ( 'NONE',  #18918 ) ;
#24712=VERTEX_POINT ( 'NONE', #11428 ) ;
#24745=CARTESIAN_POINT ( 'NONE',  ( -4.250000000000000000, 5.204748896376250699E-16, -9.449444346342714240 ) ) ;
#24769=FACE_OUTER_BOUND ( 'NONE', #28321, .T. ) ;
#24771=FACE_OUTER_BOUND ( 'NONE', #27682, .T. ) ;
#24783=ORIENTED_EDGE ( 'NONE', *, *, #20863, .T. ) ;
#24787=CARTESIAN_POINT ( 'NONE',  ( -7.500000000000000000, 4.330127018922191873, -7.422398894150032511 ) ) ;
#24792=CARTESIAN_POINT ( 'NONE',  ( -7.922281120364393914, 4.573931137438271399, -8.047472243342930653 ) ) ;
#24822=CARTESIAN_POINT ( 'NONE',  ( -6.127431526422343306E-17, 9.147862274876549904, -8.047472243342932430 ) ) ;
#24838=FACE_BOUND ( 'NONE', #26834, .T. ) ;
#24957=B_SPLINE_CURVE_WITH_KNOTS ( 'NONE', 3,
 ( #28809, #19075, #850, #29464, #23690, #13134, #21466, #18749, #26567 ),
 .UNSPECIFIED., .F., .F.,
 ( 4, 2, 1, 2, 4 ),
 ( 0.000000000000000000, 0.002165063509461097498, 0.004330127018922194995, 0.006495190528383292493, 0.008660254037844389990 ),
 .UNSPECIFIED. ) ;
#24963=ORIENTED_EDGE ( 'NONE', *, *, #11562, .F. ) ;
#24972=CARTESIAN_POINT ( 'NONE',  ( -7.499999999999998224, 1.489914625143999416, -0.1187923833806747292 ) ) ;
#24980=AXIS2_PLACEMENT_3D ( 'NONE', #23834, #30850, #7680 ) ;
#24987=LINE ( 'NONE', #16967, #4262 ) ;
#25041=VERTEX_POINT ( 'NONE', #12260 ) ;
#25072=ORIENTED_EDGE ( 'NONE', *, *, #11562, .T. ) ;
#25159=AXIS2_PLACEMENT_3D ( 'NONE', #29222, #16273, #31775 ) ;
#25245=B_SPLINE_CURVE_WITH_KNOTS ( 'NONE', 3,
 ( #3329, #3169, #10522, #7960, #24114, #20902 ),
 .UNSPECIFIED., .F., .F.,
 ( 4, 2, 4 ),
 ( -5.145455527296316946E-06, 0.0004153350442917303517, 0.0008358155441107569450 ),
 .UNSPECIFIED. ) ;
#25300=CARTESIAN_POINT ( 'NONE',  ( 7.847095227763521308, 4.129731495738485414, -7.493596212620238894 ) ) ;
#25521=CARTESIAN_POINT ( 'NONE',  ( 0.000000000000000000, 0.000000000000000000, -25.03750572909317285 ) ) ;
#25529=CARTESIAN_POINT ( 'NONE',  ( -4.250000000000000000, 5.204748896376250699E-16, -10.00000000000000000 ) ) ;
#25547=VERTEX_POINT ( 'NONE', #18555 ) ;
#25611=CARTESIAN_POINT ( 'NONE',  ( -2.352174619740013739, 7.302225387956623237, -7.450218641348505422 ) ) ;
#25636=EDGE_LOOP ( 'NONE', ( #4171, #2088, #15026, #27515 ) ) ;
#25709=CARTESIAN_POINT ( 'NONE',  ( 0.000000000000000000, 0.000000000000000000, 0.000000000000000000 ) ) ;
#25743=FACE_OUTER_BOUND ( 'NONE', #726, .T. ) ;
#25769=CARTESIAN_POINT ( 'NONE',  ( 7.500000000000000888, 3.639598441879751345, -0.7155132341745285007 ) ) ;
#25804=EDGE_CURVE ( 'NONE', #23132, #8055, #4385, .T. ) ;
#25811=VERTEX_POINT ( 'NONE', #9325 ) ;
#25820=CARTESIAN_POINT ( 'NONE',  ( 0.5974722283283632196, -8.315303285985693904, -0.7026937717022971874 ) ) ;
#25838=CARTESIAN_POINT ( 'NONE',  ( -1.282512619719133662, -8.391164935524759727, -7.795653906409117262 ) ) ;
#25862=CYLINDRICAL_SURFACE ( 'NONE', #32685, 5.000000000000000888 ) ;
#25888=DIRECTION ( 'NONE',  ( 1.000000000000000000, 0.000000000000000000, 0.000000000000000000 ) ) ;
#25957=ADVANCED_FACE ( 'NONE', ( #30973 ), #17858, .F. ) ;
#25968=DIRECTION ( 'NONE',  ( -0.000000000000000000, -0.000000000000000000, 1.000000000000000000 ) ) ;
#25980=DIRECTION ( 'NONE',  ( 0.000000000000000000, 0.000000000000000000, 1.000000000000000000 ) ) ;
#25993=DIRECTION ( 'NONE',  ( -1.000000000000000000, 0.000000000000000000, 0.000000000000000000 ) ) ;
#26005=DIRECTION ( 'NONE',  ( -0.000000000000000000, -0.000000000000000000, 1.000000000000000000 ) ) ;
#26084=CIRCLE ( 'NONE', #3746, 5.000000000000000888 ) ;
#26105=AXIS2_PLACEMENT_3D ( 'NONE', #5132, #7362, #9911 ) ;
#26110=CARTESIAN_POINT ( 'NONE',  ( 7.499999999999999112, 0.3744244963005059490, 1.526918059583750369E-15 ) ) ;
#26134=CARTESIAN_POINT ( 'NONE',  ( -7.922281120364393914, -4.573931137438277617, -8.047472243342932430 ) ) ;
#26144=CARTESIAN_POINT ( 'NONE',  ( 3.295171437449806451, 7.213553046161976567, -7.590212325761626744 ) ) ;
#26209=DIRECTION ( 'NONE',  ( 1.000000000000000000, 0.000000000000000000, -0.000000000000000000 ) ) ;
#26223=CARTESIAN_POINT ( 'NONE',  ( -6.602753909532903975, -5.319290460493544259, -7.792447862505333056 ) ) ;
#26255=ADVANCED_BREP_SHAPE_REPRESENTATION ( '', ( #12730, #2404 ), #11614 ) ;
#26261=ORIENTED_EDGE ( 'NONE', *, *, #19384, .T. ) ;
#26299=AXIS2_PLACEMENT_3D ( 'NONE', #22754, #17639, #20190 ) ;
#26342=PRODUCT_DEFINITION_CONTEXT ( 'detailed design', #21167, 'design' ) ;
#26355=CARTESIAN_POINT ( 'NONE',  ( 7.894787914004607998, 1.243647571710251278E-13, -7.591390474663425536 ) ) ;
#26359=DIRECTION ( 'NONE',  ( -1.000000000000000000, 0.000000000000000000, 0.000000000000000000 ) ) ;
#26377=ORIENTED_EDGE ( 'NONE', *, *, #20440, .T. ) ;
#26402=PRESENTATION_STYLE_ASSIGNMENT (( #13951 ) ) ;
#26452=CARTESIAN_POINT ( 'NONE',  ( 6.874999999999997335, -4.690970937165716670, -7.298562697733105509 ) ) ;
#26471=FACE_OUTER_BOUND ( 'NONE', #17129, .T. ) ;
#26502=ORIENTED_EDGE ( 'NONE', *, *, #33319, .T. ) ;
#26519=CARTESIAN_POINT ( 'NONE',  ( 1.250000000000000222, 7.938566201357357244, -7.198902722707428481 ) ) ;
#26522=CARTESIAN_POINT ( 'NONE',  ( 7.894705354777835637, 0.7527931906242791849, -7.590204373988219011 ) ) ;
#26546=EDGE_LOOP ( 'NONE', ( #21894, #6171, #31820, #3609, #24963 ) ) ;
#26558=( NAMED_UNIT ( * ) PLANE_ANGLE_UNIT ( ) SI_UNIT ( $, .RADIAN. ) );
#26561=CARTESIAN_POINT ( 'NONE',  ( 6.625705691649528717, -5.306270977113132226, -7.795653906408932521 ) ) ;
#26567=CARTESIAN_POINT ( 'NONE',  ( -7.500000000000000000, -4.330127018922198090, -7.422398894150034288 ) ) ;
#26593=CARTESIAN_POINT ( 'NONE',  ( 0.000000000000000000, 0.000000000000000000, -25.03750572909317285 ) ) ;
#26599=DIRECTION ( 'NONE',  ( 1.000000000000000000, 0.000000000000000000, 0.000000000000000000 ) ) ;
#26621=CARTESIAN_POINT ( 'NONE',  ( -7.894787914004607998, -0.7661396099416333261, -7.591390474663429089 ) ) ;
#26633=CARTESIAN_POINT ( 'NONE',  ( 7.500000000000000888, -0.7512838658081439913, 1.423015351387224570E-15 ) ) ;
#26639=SHAPE_REPRESENTATION_RELATIONSHIP ( 'NONE' , 'NONE' ,  #16098, #26255 ) ;
#26691=CARTESIAN_POINT ( 'NONE',  ( 7.922281120364393914, 4.573931137438269623, -8.047472243342930653 ) ) ;
#26700=DIRECTION ( 'NONE',  ( 0.000000000000000000, 0.000000000000000000, -1.000000000000000000 ) ) ;
#26707=ORIENTED_EDGE ( 'NONE', *, *, #6858, .F. ) ;
#26721=CARTESIAN_POINT ( 'NONE',  ( 7.922281120364393914, -4.573931137438282057, -8.047472243342932430 ) ) ;
#26736=CARTESIAN_POINT ( 'NONE',  ( -7.500000000000000888, -0.7512838658081441023, 1.307818870560639724E-15 ) ) ;
#26748=EDGE_CURVE ( 'NONE', #8055, #30882, #33033, .T. ) ;
#26758=CARTESIAN_POINT ( 'NONE',  ( 7.500000000000000000, -4.330127018922199866, -7.422398894150035176 ) ) ;
#26811=ADVANCED_FACE ( 'NONE', ( #17802 ), #2841, .F. ) ;
#26834=EDGE_LOOP ( 'NONE', ( #5100, #21396 ) ) ;
#26856=CARTESIAN_POINT ( 'NONE',  ( 4.999999999999999112, 5.773502691896256422, -7.063244554129997965 ) ) ;
#26862=CARTESIAN_POINT ( 'NONE',  ( 7.500000000000000888, -4.651016565836964212, -7.928861822685564498 ) ) ;
#26934=CARTESIAN_POINT ( 'NONE',  ( 7.922281120364393914, 4.573931137438269623, -8.047472243342930653 ) ) ;
#26955=CARTESIAN_POINT ( 'NONE',  ( -2.621328321948020346, -7.606199919102354379, -7.633618187056584681 ) ) ;
#27028=CARTESIAN_POINT ( 'NONE',  ( 7.897836333153806621, 1.530409084195003988, -7.633857274177628049 ) ) ;
#27046=EDGE_LOOP ( 'NONE', ( #16980, #22194, #24032, #32194, #21706 ) ) ;
#27057=DIRECTION ( 'NONE',  ( -1.000000000000000000, 0.000000000000000000, 0.000000000000000000 ) ) ;
#27072=CARTESIAN_POINT ( 'NONE',  ( 5.112021521198788498, -5.708827036477115868, -7.069802615102037890 ) ) ;
#27085=CARTESIAN_POINT ( 'NONE',  ( 5.000000000000000888, 0.000000000000000000, -10.00000000000000000 ) ) ;
#27119=AXIS2_PLACEMENT_3D ( 'NONE', #32084, #27474, #1084 ) ;
#27126=CARTESIAN_POINT ( 'NONE',  ( -1.305263714129178521, 8.377797850839286298, -7.792447862505335721 ) ) ;
#27211=ORIENTED_EDGE ( 'NONE', *, *, #212, .T. ) ;
#27256=ORIENTED_EDGE ( 'NONE', *, *, #25804, .F. ) ;
#27274=CARTESIAN_POINT ( 'NONE',  ( 7.500000000000000000, 2.886751345948125547, -7.198902722707427593 ) ) ;
#27280=DIRECTION ( 'NONE',  ( 1.000000000000000000, 0.000000000000000000, 0.000000000000000000 ) ) ;
#27391=ADVANCED_FACE ( 'NONE', ( #24771 ), #21071, .T. ) ;
#27394=AXIS2_PLACEMENT_3D ( 'NONE', #30534, #27632, #27800 ) ;
#27423=STYLED_ITEM ( 'NONE', ( #26402 ), #12730 ) ;
#27449=DIRECTION ( 'NONE',  ( 0.000000000000000000, 0.000000000000000000, 1.000000000000000000 ) ) ;
#27474=DIRECTION ( 'NONE',  ( 0.000000000000000000, 0.000000000000000000, -1.000000000000000000 ) ) ;
#27489=CARTESIAN_POINT ( 'NONE',  ( -2.325424218463065351, 7.317669739334662360, -7.030005583190789054 ) ) ;
#27515=ORIENTED_EDGE ( 'NONE', *, *, #22411, .F. ) ;
#27615=CARTESIAN_POINT ( 'NONE',  ( -6.127431526422343306E-17, 9.147862274876549904, -8.047472243342932430 ) ) ;
#27632=DIRECTION ( 'NONE',  ( -0.000000000000000000, -0.000000000000000000, 1.000000000000000000 ) ) ;
#27636=CARTESIAN_POINT ( 'NONE',  ( -3.750000000000007105, -6.495190528383289141, 0.000000000000000000 ) ) ;
#27650=EDGE_CURVE ( 'NONE', #16155, #14265, #27818, .T. ) ;
#27678=DIRECTION ( 'NONE',  ( 0.000000000000000000, 0.000000000000000000, 1.000000000000000000 ) ) ;
#27682=EDGE_LOOP ( 'NONE', ( #28676, #17615, #15153 ) ) ;
#27695=ADVANCED_FACE ( 'NONE', ( #22372 ), #17405, .F. ) ;
#27699=CARTESIAN_POINT ( 'NONE',  ( -7.500000000000005329, 4.330127018922187432, -7.564335161054492218 ) ) ;
#27705=PRODUCT_DEFINITION ( 'UNKNOWN', '', #9395, #26342 ) ;
#27747=CARTESIAN_POINT ( 'NONE',  ( 6.902527771671632451, 4.675077770780898589, -0.7026937717022819774 ) ) ;
#27787=CARTESIAN_POINT ( 'NONE',  ( -6.601567268551443490, 5.319966374295965750, -7.792327460285856766 ) ) ;
#27790=ORIENTED_EDGE ( 'NONE', *, *, #27650, .F. ) ;
#27800=DIRECTION ( 'NONE',  ( 1.000000000000000000, 0.000000000000000000, 0.000000000000000000 ) ) ;
#27806=VERTEX_POINT ( 'NONE', #12326 ) ;
#27818=LINE ( 'NONE', #28172, #3676 ) ;
#27846=CARTESIAN_POINT ( 'NONE',  ( 0.000000000000000000, 0.000000000000000000, -8.499999999999998224 ) ) ;
#27897=DIRECTION ( 'NONE',  ( -0.000000000000000000, -0.000000000000000000, 1.000000000000000000 ) ) ;
#27907=DIRECTION ( 'NONE',  ( 1.000000000000000000, 0.000000000000000000, 0.000000000000000000 ) ) ;
#27962=CARTESIAN_POINT ( 'NONE',  ( -3.749999999999998224, -6.495190528383296247, -6.991905250253752868 ) ) ;
#27986=CIRCLE ( 'NONE', #17093, 10.12668159690567649 ) ;
#27997=CARTESIAN_POINT ( 'NONE',  ( -7.848314987057850800, 4.129027267381560229, -7.493854785173809319 ) ) ;
#28022=ORIENTED_EDGE ( 'NONE', *, *, #29470, .F. ) ;
#28025=CARTESIAN_POINT ( 'NONE',  ( -7.500000000000000000, 4.330127018922191873, -0.9999999999999970024 ) ) ;
#28054=B_SPLINE_CURVE_WITH_KNOTS ( 'NONE', 3,
 ( #19858, #30256, #6918, #17309, #27699, #4361 ),
 .UNSPECIFIED., .F., .F.,
 ( 4, 2, 4 ),
 ( -5.145455527297706927E-06, 0.0004153350442917282917, 0.0008358155441107560776 ),
 .UNSPECIFIED. ) ;
#28064=DIRECTION ( 'NONE',  ( -0.000000000000000000, -0.000000000000000000, 1.000000000000000000 ) ) ;
#28073=DIRECTION ( 'NONE',  ( 1.000000000000000000, 0.000000000000000000, 0.000000000000000000 ) ) ;
#28095=VECTOR ( 'NONE', #9568, 1000.000000000000000 ) ;
#28112=CARTESIAN_POINT ( 'NONE',  ( 0.000000000000000000, 0.000000000000000000, 0.000000000000000000 ) ) ;
#28120=PRODUCT_CONTEXT ( 'NONE', #13745, 'mechanical' ) ;
#28135=ORIENTED_EDGE ( 'NONE', *, *, #8078, .T. ) ;
#28150=CIRCLE ( 'NONE', #33600, 4.250000000000000000 ) ;
#28172=CARTESIAN_POINT ( 'NONE',  ( -5.000000000000001776, 0.000000000000000000, -9.974600000000000577 ) ) ;
#28180=CARTESIAN_POINT ( 'NONE',  ( 7.500000000000000000, 4.330127018922190096, -7.422398894150032511 ) ) ;
#28194=CARTESIAN_POINT ( 'NONE',  ( 4.336808689942017736E-16, 8.660254037844390851, -1.000000000000000888 ) ) ;
#28250=FACE_OUTER_BOUND ( 'NONE', #22690, .T. ) ;
#28291=CARTESIAN_POINT ( 'NONE',  ( 4.406842699996126989, -6.115962218725295330, -6.291760732204942919E-15 ) ) ;
#28293=CARTESIAN_POINT ( 'NONE',  ( -1.306442393143578462, -8.377108146505394259, -7.792327460285862983 ) ) ;
#28305=CARTESIAN_POINT ( 'NONE',  ( -0.04606493828583551470, -9.175055303659563677, -8.057411785091794343 ) ) ;
#28321=EDGE_LOOP ( 'NONE', ( #17633, #9413, #4753 ) ) ;
#28365=ORIENTED_EDGE ( 'NONE', *, *, #23511, .F. ) ;
#28407=CARTESIAN_POINT ( 'NONE',  ( -4.403473400622099909, -6.117907484625868975, -5.839445138371144960E-15 ) ) ;
#28410=CARTESIAN_POINT ( 'NONE',  ( -7.500000000000000000, -0.7729939684941458111, -7.026407045654831762 ) ) ;
#28441=DIRECTION ( 'NONE',  ( 0.000000000000000000, 0.000000000000000000, -1.000000000000000000 ) ) ;
#28448=CARTESIAN_POINT ( 'NONE',  ( 0.000000000000000000, 0.000000000000000000, 0.000000000000000000 ) ) ;
#28455=CARTESIAN_POINT ( 'NONE',  ( 3.750000000000004441, -6.495190528383289141, 0.000000000000000000 ) ) ;
#28487=CIRCLE ( 'NONE', #23593, 5.000000000000001776 ) ;
#28521=ORIENTED_EDGE ( 'NONE', *, *, #2302, .T. ) ;
#28537=( GEOMETRIC_REPRESENTATION_CONTEXT ( 3 ) GLOBAL_UNCERTAINTY_ASSIGNED_CONTEXT ( ( #10685 ) ) GLOBAL_UNIT_ASSIGNED_CONTEXT ( ( #29632, #26558, #31840 ) ) REPRESENTATION_CONTEXT ( 'NONE', 'WORKASPACE' ) );
#28615=CARTESIAN_POINT ( 'NONE',  ( -7.914984360234579519, 3.818534719232089980, -7.907701344400639876 ) ) ;
#28632=CARTESIAN_POINT ( 'NONE',  ( -3.750000000000004885, 6.495190528383289141, 0.000000000000000000 ) ) ;
#28639=DIRECTION ( 'NONE',  ( -0.8660254037844382635, 0.5000000000000005551, 0.000000000000000000 ) ) ;
#28676=ORIENTED_EDGE ( 'NONE', *, *, #7885, .F. ) ;
#28681=ADVANCED_FACE ( 'NONE', ( #12621 ), #4961, .F. ) ;
#28711=ADVANCED_FACE ( 'NONE', ( #28963 ), #24570, .F. ) ;
#28745=CARTESIAN_POINT ( 'NONE',  ( -7.897827455343210623, -1.533134349199909208, -7.633632140068262295 ) ) ;
#28776=EDGE_LOOP ( 'NONE', ( #20017, #21384, #17759, #159, #29813, #18834, #15144 ) ) ;
#28809=CARTESIAN_POINT ( 'NONE',  ( -7.500000000000000000, 4.330127018922191873, -7.422398894150032511 ) ) ;
#28827=ORIENTED_EDGE ( 'NONE', *, *, #6811, .F. ) ;
#28829=CARTESIAN_POINT ( 'NONE',  ( 7.500000000000001776, 0.000000000000000000, 0.000000000000000000 ) ) ;
#28862=CARTESIAN_POINT ( 'NONE',  ( 7.500000000000000888, -3.640541674360523228, -0.7158139487964624292 ) ) ;
#28876=ORIENTED_EDGE ( 'NONE', *, *, #5778, .F. ) ;
#28903=B_SPLINE_CURVE_WITH_KNOTS ( 'NONE', 3,
 ( #13738, #18854, #32133, #29415, #21246, #3190 ),
 .UNSPECIFIED., .F., .F.,
 ( 4, 2, 4 ),
 ( 2.475503369212747145E-07, 0.002222330217055634109, 0.004444412883774346255 ),
 .UNSPECIFIED. ) ;
#28920=CARTESIAN_POINT ( 'NONE',  ( 7.914973979435151463, 3.817460047930444134, -7.907502498112419786 ) ) ;
#28951=CARTESIAN_POINT ( 'NONE',  ( -2.621086668468698644, -7.606368536631371136, -7.634085501268427443 ) ) ;
#28963=FACE_OUTER_BOUND ( 'NONE', #25636, .T. ) ;
#28991=EDGE_LOOP ( 'NONE', ( #16516, #24537, #13468, #88, #24783 ) ) ;
#29160=CARTESIAN_POINT ( 'NONE',  ( 7.500000000000000000, 4.330127018922190096, -7.422398894150032511 ) ) ;
#29186=B_SPLINE_CURVE_WITH_KNOTS ( 'NONE', 3,
 ( #20126, #30520, #22855, #12290, #27962, #7185, #4452, #2075, #33246 ),
 .UNSPECIFIED., .F., .F.,
 ( 4, 2, 1, 2, 4 ),
 ( 0.000000000000000000, 0.002165063509461097064, 0.004330127018922194128, 0.006495190528383290758, 0.008660254037844389990 ),
 .UNSPECIFIED. ) ;
#29222=CARTESIAN_POINT ( 'NONE',  ( -2.352990130084580066E-16, 8.660254037844390851, -10.00000000000000000 ) ) ;
#29254=CARTESIAN_POINT ( 'NONE',  ( 7.499999999997997158, -3.157198044624895061, -7.642795354507847527 ) ) ;
#29312=ORIENTED_EDGE ( 'NONE', *, *, #12524, .T. ) ;
#29322=EDGE_CURVE ( 'NONE', #16155, #31786, #30649, .T. ) ;
#29352=CARTESIAN_POINT ( 'NONE',  ( -1.013163106016700565, -8.075304045852661261, -7.231838333420565590 ) ) ;
#29356=CARTESIAN_POINT ( 'NONE',  ( -7.894787914004607998, -1.230850257101226302E-13, -7.591390474663425536 ) ) ;
#29397=FACE_OUTER_BOUND ( 'NONE', #11683, .T. ) ;
#29415=CARTESIAN_POINT ( 'NONE',  ( 2.452879891156805492, 7.244083172395185954, -0.1007566405101774504 ) ) ;
#29459=CARTESIAN_POINT ( 'NONE',  ( 7.169303301815196150, -4.521054846639319003, -7.349897473155491134 ) ) ;
#29464=CARTESIAN_POINT ( 'NONE',  ( -7.499999999999999112, 1.443375672974061219, -7.063244554130000630 ) ) ;
#29470=EDGE_CURVE ( 'NONE', #2927, #33504, #11035, .T. ) ;
#29479=VERTEX_POINT ( 'NONE', #21417 ) ;
#29490=DIRECTION ( 'NONE',  ( 0.000000000000000000, 0.000000000000000000, 1.000000000000000000 ) ) ;
#29491=ADVANCED_FACE ( 'NONE', ( #8155 ), #10460, .F. ) ;
#29497=EDGE_CURVE ( 'NONE', #613, #22909, #31596, .T. ) ;
#29513=CARTESIAN_POINT ( 'NONE',  ( -5.174575781537456010, -5.672711317431625488, -7.030005583190790830 ) ) ;
#29623=CARTESIAN_POINT ( 'NONE',  ( -3.823040241140506157E-16, -8.660254037844397956, -7.564338275809345369 ) ) ;
#29632=( LENGTH_UNIT ( ) NAMED_UNIT ( * ) SI_UNIT ( .MILLI., .METRE. ) );
#29682=EDGE_CURVE ( 'NONE', #12471, #22574, #24987, .T. ) ;
#29731=ORIENTED_EDGE ( 'NONE', *, *, #17084, .F. ) ;
#29751=CARTESIAN_POINT ( 'NONE',  ( 0.000000000000000000, 0.000000000000000000, 0.000000000000000000 ) ) ;
#29766=CONICAL_SURFACE ( 'NONE', #17243, 7.500000000000001776, 0.8594454914424796144 ) ;
#29808=DIRECTION ( 'NONE',  ( 0.000000000000000000, 0.000000000000000000, 1.000000000000000000 ) ) ;
#29813=ORIENTED_EDGE ( 'NONE', *, *, #17958, .T. ) ;
#29844=CARTESIAN_POINT ( 'NONE',  ( -7.703920929261754758, -4.447860822324869901, -7.917989418073284824 ) ) ;
#30022=EDGE_LOOP ( 'NONE', ( #6943, #32488, #22140, #15901, #27211 ) ) ;
#30046=CARTESIAN_POINT ( 'NONE',  ( 0.2779000157839532359, 8.820699686765054892, -7.928862157988302961 ) ) ;
#30052=CONICAL_SURFACE ( 'NONE', #21339, 7.500000000000001776, 0.8594454914424796144 ) ;
#30076=CONICAL_SURFACE ( 'NONE', #9979, 10.39117206796836079, 1.221730476396047926 ) ;
#30178=DIRECTION ( 'NONE',  ( 1.000000000000000000, 0.000000000000000000, 0.000000000000000000 ) ) ;
#30192=LINE ( 'NONE', #14848, #28095 ) ;
#30256=CARTESIAN_POINT ( 'NONE',  ( -7.808218555861951238, 4.508077085120201666, -7.999534413642737540 ) ) ;
#30367=EDGE_CURVE ( 'NONE', #1999, #25547, #29186, .T. ) ;
#30412=EDGE_CURVE ( 'NONE', #17539, #25041, #10753, .T. ) ;
#30414=AXIS2_PLACEMENT_3D ( 'NONE', #19102, #29490, #24383 ) ;
#30519=PLANE ( 'NONE',  #32606 ) ;
#30520=CARTESIAN_POINT ( 'NONE',  ( -6.875000000000001776, -4.690970937165714894, -7.298562697733108173 ) ) ;
#30534=CARTESIAN_POINT ( 'NONE',  ( 0.000000000000000000, 0.000000000000000000, 0.000000000000000000 ) ) ;
#30557=CARTESIAN_POINT ( 'NONE',  ( -6.625705691649848461, 5.306270977113102916, -7.795653906409009792 ) ) ;
#30566=B_SPLINE_CURVE_WITH_KNOTS ( 'NONE', 3,
 ( #23348, #30681, #10244, #7678, #28291, #28455 ),
 .UNSPECIFIED., .F., .F.,
 ( 4, 2, 4 ),
 ( 2.475503369227215526E-07, 0.002222330217055624568, 0.004444412883774326306 ),
 .UNSPECIFIED. ) ;
#30575=CARTESIAN_POINT ( 'NONE',  ( -1.211595439868048629, 7.960739084487649109, -0.4504974108211966533 ) ) ;
#30584=EDGE_LOOP ( 'NONE', ( #19041, #14098, #20050, #26261 ) ) ;
#30586=CIRCLE ( 'NONE', #1732, 5.000000000000000888 ) ;
#30589=CARTESIAN_POINT ( 'NONE',  ( -7.500000000000000000, 0.7513028741560130452, -0.02472015219302865774 ) ) ;
#30591=EDGE_CURVE ( 'NONE', #2685, #3624, #1036, .T. ) ;
#30599=CARTESIAN_POINT ( 'NONE',  ( -2.352990130084580066E-16, 8.660254037844390851, -7.422398894150034288 ) ) ;
#30622=B_SPLINE_CURVE_WITH_KNOTS ( 'NONE', 3,
 ( #33128, #9794, #20178, #30575, #7237, #17625 ),
 .UNSPECIFIED., .F., .F.,
 ( 4, 2, 4 ),
 ( 0.004444412883774334112, 0.006655097293744431999, 0.008865781703714530754 ),
 .UNSPECIFIED. ) ;
#30633=ORIENTED_EDGE ( 'NONE', *, *, #18880, .F. ) ;
#30649=LINE ( 'NONE', #25529, #4807 ) ;
#30681=CARTESIAN_POINT ( 'NONE',  ( 6.901579824520443829, -4.675625068323827627, -0.7022220667781372549 ) ) ;
#30794=EDGE_CURVE ( 'NONE', #16934, #854, #23893, .T. ) ;
#30806=CARTESIAN_POINT ( 'NONE',  ( 0.000000000000000000, 0.000000000000000000, -9.226681596905677907 ) ) ;
#30832=ORIENTED_EDGE ( 'NONE', *, *, #7885, .T. ) ;
#30850=DIRECTION ( 'NONE',  ( -0.5000000000000008882, -0.8660254037844382635, 0.000000000000000000 ) ) ;
#30882=VERTEX_POINT ( 'NONE', #14868 ) ;
#30891=ORIENTED_EDGE ( 'NONE', *, *, #32268, .T. ) ;
#30933=DIRECTION ( 'NONE',  ( 1.000000000000000000, 0.000000000000000000, 0.000000000000000000 ) ) ;
#30938=CARTESIAN_POINT ( 'NONE',  ( 2.459698528280935825, -7.240146430416073642, -0.09933465333851955459 ) ) ;
#30943=CARTESIAN_POINT ( 'NONE',  ( -6.250000000000000888, 5.051814855409225480, -7.198902722707429369 ) ) ;
#30948=ADVANCED_FACE ( 'NONE', ( #1930 ), #10167, .F. ) ;
#30973=FACE_OUTER_BOUND ( 'NONE', #13155, .T. ) ;
#30982=CIRCLE ( 'NONE', #13546, 7.500000000000001776 ) ;
#31032=CARTESIAN_POINT ( 'NONE',  ( -2.352990130084580066E-16, 8.660254037844390851, -7.422398894150034288 ) ) ;
#31100=DIRECTION ( 'NONE',  ( 0.000000000000000000, 0.000000000000000000, 1.000000000000000000 ) ) ;
#31134=CARTESIAN_POINT ( 'NONE',  ( -7.500000000000000000, -3.882691789160215290, -7.781695678273567118 ) ) ;
#31168=CARTESIAN_POINT ( 'NONE',  ( -7.897850199329715437, 1.533397866934075759, -7.634054012537968781 ) ) ;
#31182=VECTOR ( 'NONE', #27678, 1000.000000000000000 ) ;
#31192=CARTESIAN_POINT ( 'NONE',  ( -5.047120108843199837, 5.746297884371392328, -0.1007566405101777279 ) ) ;
#31274=SURFACE_STYLE_FILL_AREA ( #2656 ) ;
#31280=CARTESIAN_POINT ( 'NONE',  ( 0.000000000000000000, 0.000000000000000000, -10.00000000000000000 ) ) ;
#31305=CARTESIAN_POINT ( 'NONE',  ( -7.894955577759523280, 1.603085139988202901, -7.593799241562120272 ) ) ;
#31368=ORIENTED_EDGE ( 'NONE', *, *, #1176, .F. ) ;
#31418=VERTEX_POINT ( 'NONE', #20412 ) ;
#31433=FILL_AREA_STYLE_COLOUR ( '', #21406 ) ;
#31443=CARTESIAN_POINT ( 'NONE',  ( -6.874999999999995559, 4.690970937165706900, -7.298562697733101068 ) ) ;
#31476=CONICAL_SURFACE ( 'NONE', #27119, 7.500000000000001776, 0.8594454914424796144 ) ;
#31488=CARTESIAN_POINT ( 'NONE',  ( 5.000000000000001776, 6.123233995736768255E-16, -9.974600000000000577 ) ) ;
#31505=CARTESIAN_POINT ( 'NONE',  ( -7.894787914004607998, 0.7647108141804108694, -7.591390474663421095 ) ) ;
#31541=ORIENTED_EDGE ( 'NONE', *, *, #16321, .T. ) ;
#31572=CARTESIAN_POINT ( 'NONE',  ( 2.499999999999999112, -7.216878364870334295, -7.063244554130005959 ) ) ;
#31596=B_SPLINE_CURVE_WITH_KNOTS ( 'NONE', 3,
 ( #26691, #28920, #13742, #27028, #18703, #24139 ),
 .UNSPECIFIED., .F., .F.,
 ( 4, 2, 4 ),
 ( 0.000000000000000000, 0.002307655110370371299, 0.004615310220740742597 ),
 .UNSPECIFIED. ) ;
#31617=ORIENTED_EDGE ( 'NONE', *, *, #32432, .F. ) ;
#31618=EDGE_CURVE ( 'NONE', #22909, #948, #16922, .T. ) ;
#31672=CARTESIAN_POINT ( 'NONE',  ( -4.232971792145048787E-15, -9.016621985895911351, -7.999704684617487516 ) ) ;
#31713=DIRECTION ( 'NONE',  ( -0.000000000000000000, -0.000000000000000000, 1.000000000000000000 ) ) ;
#31733=CARTESIAN_POINT ( 'NONE',  ( -3.093533885184598375, -6.874201416485457017, -7.446478553994068328 ) ) ;
#31749=CARTESIAN_POINT ( 'NONE',  ( -0.04725809328185606034, 9.175759667312519241, -8.057670357645360326 ) ) ;
#31775=DIRECTION ( 'NONE',  ( -0.8660254037844382635, -0.5000000000000004441, 0.000000000000000000 ) ) ;
#31786=VERTEX_POINT ( 'NONE', #18359 ) ;
#31800=CARTESIAN_POINT ( 'NONE',  ( 7.500000000000000000, 4.330127018922190096, -7.422398894150032511 ) ) ;
#31820=ORIENTED_EDGE ( 'NONE', *, *, #29497, .F. ) ;
#31834=CARTESIAN_POINT ( 'NONE',  ( 7.264118654998712898, -4.945491722146229563, -7.907633014911220393 ) ) ;
#31840=( NAMED_UNIT ( * ) SI_UNIT ( $, .STERADIAN. ) SOLID_ANGLE_UNIT ( ) );
#31843=CARTESIAN_POINT ( 'NONE',  ( 7.848314987057850800, -4.129027267381569999, -7.493854785173811095 ) ) ;
#31873=DIRECTION ( 'NONE',  ( 1.000000000000000000, 0.000000000000000000, 0.000000000000000000 ) ) ;
#31891=CARTESIAN_POINT ( 'NONE',  ( 0.000000000000000000, 0.000000000000000000, 0.000000000000000000 ) ) ;
#31961=DIRECTION ( 'NONE',  ( 0.000000000000000000, 0.000000000000000000, -1.000000000000000000 ) ) ;
#31981=FACE_OUTER_BOUND ( 'NONE', #21432, .T. ) ;
#32014=CARTESIAN_POINT ( 'NONE',  ( 7.112481253774308954, -4.553861071371678726, -7.781689322728511549 ) ) ;
#32047=CARTESIAN_POINT ( 'NONE',  ( 7.500000000000000888, 4.330127018922190985, -7.564338275809340928 ) ) ;
#32071=CARTESIAN_POINT ( 'NONE',  ( -5.147825380260782957, -5.688155668810408017, -7.450218641351304960 ) ) ;
#32084=CARTESIAN_POINT ( 'NONE',  ( 0.000000000000000000, 0.000000000000000000, 0.000000000000000000 ) ) ;
#32133=CARTESIAN_POINT ( 'NONE',  ( 1.206569728928466700, 7.963640680051486953, -0.4524126574264497602 ) ) ;
#32146=CARTESIAN_POINT ( 'NONE',  ( 7.922281120364393914, 4.573931137438269623, -8.047472243342930653 ) ) ;
#32165=CARTESIAN_POINT ( 'NONE',  ( -7.297096662748653293E-16, -8.716842316802402735, -7.700127545397317697 ) ) ;
#32175=FILL_AREA_STYLE_COLOUR ( '', #1869 ) ;
#32194=ORIENTED_EDGE ( 'NONE', *, *, #9929, .T. ) ;
#32263=VERTEX_POINT ( 'NONE', #21626 ) ;
#32268=EDGE_CURVE ( 'NONE', #27806, #21434, #15333, .T. ) ;
#32274=VECTOR ( 'NONE', #25980, 1000.000000000000000 ) ;
#32333=DIRECTION ( 'NONE',  ( 1.000000000000000000, 0.000000000000000000, -0.000000000000000000 ) ) ;
#32373=ORIENTED_EDGE ( 'NONE', *, *, #13038, .F. ) ;
#32432=EDGE_CURVE ( 'NONE', #32263, #19301, #18601, .T. ) ;
#32488=ORIENTED_EDGE ( 'NONE', *, *, #6858, .T. ) ;
#32533=ORIENTED_EDGE ( 'NONE', *, *, #32432, .T. ) ;
#32535=DIRECTION ( 'NONE',  ( 0.8660254037844382635, 0.5000000000000004441, 0.000000000000000000 ) ) ;
#32606=AXIS2_PLACEMENT_3D ( 'NONE', #7866, #22854, #28639 ) ;
#32629=CARTESIAN_POINT ( 'NONE',  ( -7.500000000000001776, 2.932633423934442263, -0.4709827563909292358 ) ) ;
#32658=EDGE_CURVE ( 'NONE', #2927, #12471, #19406, .T. ) ;
#32685=AXIS2_PLACEMENT_3D ( 'NONE', #25521, #7643, #28073 ) ;
#32727=CARTESIAN_POINT ( 'NONE',  ( -10.39117206796836257, 1.272551561242683764E-15, -8.499999999999998224 ) ) ;
#32761=CARTESIAN_POINT ( 'NONE',  ( 0.04606493828584144051, 9.175055303659556571, -8.057411785091790790 ) ) ;
#32794=CARTESIAN_POINT ( 'NONE',  ( -7.500000000000000888, 3.988838049906426875, -0.8529248949437632232 ) ) ;
#32831=VECTOR ( 'NONE', #29808, 1000.000000000000000 ) ;
#32841=CARTESIAN_POINT ( 'NONE',  ( 10.39117206796836079, 1.272551561242683567E-15, -8.499999999999998224 ) ) ;
#32964=CARTESIAN_POINT ( 'NONE',  ( -7.500000000000000888, 3.639598441879742907, -0.7155132341745253921 ) ) ;
#33019=EDGE_CURVE ( 'NONE', #21434, #25041, #33629, .T. ) ;
#33033=CIRCLE ( 'NONE', #2583, 10.39117206796836079 ) ;
#33034=ORIENTED_EDGE ( 'NONE', *, *, #30367, .F. ) ;
#33051=DIRECTION ( 'NONE',  ( 0.000000000000000000, 0.000000000000000000, -1.000000000000000000 ) ) ;
#33110=CARTESIAN_POINT ( 'NONE',  ( -5.112021521198522933, 5.708827036477257977, -7.069802615102034338 ) ) ;
#33128=CARTESIAN_POINT ( 'NONE',  ( -3.750000000000004885, 6.495190528383289141, 0.000000000000000000 ) ) ;
#33140=EDGE_CURVE ( 'NONE', #30882, #8055, #14333, .T. ) ;
#33171=B_SPLINE_CURVE_WITH_KNOTS ( 'NONE', 3,
 ( #26758, #3422, #3591, #13984, #16124, #1131 ),
 .UNSPECIFIED., .F., .F.,
 ( 4, 2, 4 ),
 ( 0.000000000000000000, 0.0004189869898914143787, 0.0008379739797828287574 ),
 .UNSPECIFIED. ) ;
#33246=CARTESIAN_POINT ( 'NONE',  ( -5.007715329123872641E-16, -8.660254037844399733, -7.422398894150038728 ) ) ;
#33257=ORIENTED_EDGE ( 'NONE', *, *, #1176, .T. ) ;
#33319=EDGE_CURVE ( 'NONE', #1999, #27806, #20871, .T. ) ;
#33402=FACE_OUTER_BOUND ( 'NONE', #18621, .T. ) ;
#33410=CARTESIAN_POINT ( 'NONE',  ( -6.901579824520442941, 4.675625068323816080, -0.7022220667781327030 ) ) ;
#33413=CARTESIAN_POINT ( 'NONE',  ( -0.3470952277635217520, -8.860649561028104415, -7.493596212620245112 ) ) ;
#33420=ORIENTED_EDGE ( 'NONE', *, *, #33140, .T. ) ;
#33439=CARTESIAN_POINT ( 'NONE',  ( 7.500000000000000888, 2.932633423934449812, -0.4709827563909316783 ) ) ;
#33450=EDGE_CURVE ( 'NONE', #25547, #19912, #5364, .T. ) ;
#33504=VERTEX_POINT ( 'NONE', #2980 ) ;
#33548=FACE_OUTER_BOUND ( 'NONE', #20601, .T. ) ;
#33600=AXIS2_PLACEMENT_3D ( 'NONE', #13235, #28064, #10192 ) ;
#33629=B_SPLINE_CURVE_WITH_KNOTS ( 'NONE', 3,
 ( #14571, #22402, #30589, #24972, #1626, #12016, #32629, #32964, #32794, #28025 ),
 .UNSPECIFIED., .F., .F.,
 ( 4, 2, 2, 2, 4 ),
 ( 0.01051144076094934904, 0.01162027323572610918, 0.01272910571050286932, 0.01383793818527962946, 0.01494677066005638960 ),
 .UNSPECIFIED. ) ;
#33654=( NAMED_UNIT ( * ) SI_UNIT ( $, .STERADIAN. ) SOLID_ANGLE_UNIT ( ) );
#33658=B_SPLINE_CURVE_WITH_KNOTS ( 'NONE', 3,
 ( #11120, #13829, #29844, #3267, #24391, #22002 ),
 .UNSPECIFIED., .F., .F.,
 ( 4, 2, 4 ),
 ( -5.145455527293010977E-06, 0.0004153350442917342006, 0.0008358155441107593302 ),
 .UNSPECIFIED. ) ;
#33662=DIRECTION ( 'NONE',  ( -0.000000000000000000, -0.000000000000000000, -1.000000000000000000 ) ) ;
#33684=ADVANCED_FACE ( 'NONE', ( #26471 ), #22531, .T. ) ;
ENDSEC;
END-ISO-10303-21;
